ISO-10303-21;
HEADER;
FILE_DESCRIPTION (('STEP AP214'),
    '1' );
FILE_NAME ('Housing Torx Attachment Screw.step',
    '2026-10-09T13:19:41',
    ( '' ),
    ( '' ),
    'SwSTEP 2.0',
    'SolidWorks 2026',
    '' );
FILE_SCHEMA (( 'AUTOMOTIVE_DESIGN' ));
ENDSEC;

DATA;
#19=ADVANCED_FACE ( 'NONE', ( #21694 ), #5826, .T. ) ;
#38=ORIENTED_EDGE ( 'NONE', *, *, #11460, .T. ) ;
#46=CONICAL_SURFACE ( 'NONE', #14894, 2.000000000000000888, 1.308996938999999804 ) ;
#72=CARTESIAN_POINT ( 'NONE',  ( -37.59243475499999931, -65.56519245710001087, -0.6307174998519999853 ) ) ;
#109=CARTESIAN_POINT ( 'NONE',  ( -40.50000000000000000, -63.30468293320000583, -2.309401076760000393 ) ) ;
#119=CYLINDRICAL_SURFACE ( 'NONE', #23798, 4.999999999999999112 ) ;
#121=PRODUCT_DEFINITION ( 'UNKNOWN', '', #18568, #21393 ) ;
#135=ORIENTED_EDGE ( 'NONE', *, *, #7062, .T. ) ;
#136=CARTESIAN_POINT ( 'NONE',  ( -40.00000000000000000, -69.00000000000000000, 0.000000000000000000 ) ) ;
#140=CARTESIAN_POINT ( 'NONE',  ( -39.22207447329392238, -63.24690319806988725, -2.469861454400793299 ) ) ;
#156=ORIENTED_EDGE ( 'NONE', *, *, #2664, .T. ) ;
#163=CARTESIAN_POINT ( 'NONE',  ( -38.62700573890000300, -65.19264941160000149, 2.813424548380000001 ) ) ;
#167=CIRCLE ( 'NONE', #27093, 2.000000000000001776 ) ;
#201=EDGE_CURVE ( 'NONE', #9396, #9232, #7255, .T. ) ;
#230=ORIENTED_EDGE ( 'NONE', *, *, #12077, .T. ) ;
#251=B_SPLINE_CURVE_WITH_KNOTS ( 'NONE', 3,
 ( #2695, #18425, #27024, #971, #16075, #16523, #22510, #7208, #16373, #25420, #27617 ),
 .UNSPECIFIED., .F., .F.,
 ( 4, 2, 1, 2, 2, 4 ),
 ( 0.000000000000000000, 0.2499999999999618638, 0.3749999999999487632, 0.4374999999999482636, 0.4999999999999477085, 1.000000000000000000 ),
 .UNSPECIFIED. ) ;
#259=DIRECTION ( 'NONE',  ( 1.000000000000000000, 0.000000000000000000, 0.000000000000000000 ) ) ;
#326=DIRECTION ( 'NONE',  ( 1.000000000000000000, 0.000000000000000000, 0.000000000000000000 ) ) ;
#339=CARTESIAN_POINT ( 'NONE',  ( -38.15937129994918564, -63.35495516230771074, -1.162516276375642921 ) ) ;
#354=ORIENTED_EDGE ( 'NONE', *, *, #12243, .F. ) ;
#356=DIRECTION ( 'NONE',  ( 0.000000000000000000, 1.000000000000000000, 0.000000000000000000 ) ) ;
#366=ORIENTED_EDGE ( 'NONE', *, *, #9045, .T. ) ;
#371=CARTESIAN_POINT ( 'NONE',  ( -36.70028666173043774, -63.05366661935808992, 0.03681143521525633011 ) ) ;
#376=CARTESIAN_POINT ( 'NONE',  ( -38.31826369283189848, -63.05366661936042050, -2.839229858537526852 ) ) ;
#377=CONICAL_SURFACE ( 'NONE', #5926, 2.000000000000000888, 1.308996938999999804 ) ;
#488=ORIENTED_EDGE ( 'NONE', *, *, #1371, .F. ) ;
#492=ORIENTED_EDGE ( 'NONE', *, *, #28617, .F. ) ;
#506=CARTESIAN_POINT ( 'NONE',  ( -43.20000000000000284, -65.14977478849999670, 0.1732050807559999961 ) ) ;
#507=B_SPLINE_CURVE_WITH_KNOTS ( 'NONE', 3,
 ( #4002, #15340, #26308, #12728 ),
 .UNSPECIFIED., .F., .F.,
 ( 4, 4 ),
 ( 0.000000000000000000, 1.000000000000000000 ),
 .UNSPECIFIED. ) ;
#555=CARTESIAN_POINT ( 'NONE',  ( -40.00000000000000000, -65.00000000000000000, 3.175426480540000096 ) ) ;
#623=VERTEX_POINT ( 'NONE', #3318 ) ;
#638=CYLINDRICAL_SURFACE ( 'NONE', #9269, 4.999999999999999112 ) ;
#646=VECTOR ( 'NONE', #958, 1000.000000000000000 ) ;
#651=VECTOR ( 'NONE', #20044, 1000.000000000000114 ) ;
#664=CARTESIAN_POINT ( 'NONE',  ( -43.22799762839635918, -65.13413837705087417, 0.1570406424686417168 ) ) ;
#665=CARTESIAN_POINT ( 'NONE',  ( -36.74605004467864688, -63.06523941402065958, -0.1332336900803410829 ) ) ;
#718=ORIENTED_EDGE ( 'NONE', *, *, #26083, .T. ) ;
#720=LINE ( 'NONE', #20953, #7524 ) ;
#748=CARTESIAN_POINT ( 'NONE',  ( -40.00000000000000000, -63.00000000000000000, 0.000000000000000000 ) ) ;
#767=VERTEX_POINT ( 'NONE', #4884 ) ;
#790=VERTEX_POINT ( 'NONE', #2415 ) ;
#813=VERTEX_POINT ( 'NONE', #16669 ) ;
#833=CARTESIAN_POINT ( 'NONE',  ( -43.20000000000000284, -64.11445222650000630, 0.1732050807559999961 ) ) ;
#846=CYLINDRICAL_SURFACE ( 'NONE', #3859, 0.9999999999999991118 ) ;
#855=DIRECTION ( 'NONE',  ( 0.5000000000001882938, 0.000000000000000000, 0.8660254037843300168 ) ) ;
#888=LINE ( 'NONE', #4938, #18082 ) ;
#891=ORIENTED_EDGE ( 'NONE', *, *, #7329, .T. ) ;
#933=B_SPLINE_CURVE_WITH_KNOTS ( 'NONE', 5,
 ( #6402, #24190, #13248, #15129, #17199, #26088, #4076, #19520, #22155 ),
 .UNSPECIFIED., .F., .F.,
 ( 6, 3, 6 ),
 ( 0.000000000000000000, 1.237573681340000009, 1.566718891480000098 ),
 .UNSPECIFIED. ) ;
#936=CARTESIAN_POINT ( 'NONE',  ( -38.20072243471708617, -65.72601415636297872, 1.277196024491957571 ) ) ;
#938=EDGE_CURVE ( 'NONE', #813, #6598, #26153, .T. ) ;
#945=ORIENTED_EDGE ( 'NONE', *, *, #24505, .F. ) ;
#951=ORIENTED_EDGE ( 'NONE', *, *, #1960, .T. ) ;
#958=DIRECTION ( 'NONE',  ( -0.7600087925152557711, 0.5000000000001688649, -0.4151946956541399114 ) ) ;
#965=ORIENTED_EDGE ( 'NONE', *, *, #6007, .F. ) ;
#971=CARTESIAN_POINT ( 'NONE',  ( -38.00203752171322691, -65.72812580224879753, 0.9281902028072916977 ) ) ;
#990=CARTESIAN_POINT ( 'NONE',  ( -41.75000000000000000, -65.14977478849999670, -2.684678751739999925 ) ) ;
#1025=B_SPLINE_CURVE_WITH_KNOTS ( 'NONE', 3,
 ( #4760, #6803, #13636, #19749, #20338, #2286 ),
 .UNSPECIFIED., .F., .F.,
 ( 4, 2, 4 ),
 ( 0.000000000000000000, 0.5000000000000000000, 1.000000000000000000 ),
 .UNSPECIFIED. ) ;
#1059=AXIS2_PLACEMENT_3D ( 'NONE', #10540, #19604, #15069 ) ;
#1084=B_SPLINE_CURVE_WITH_KNOTS ( 'NONE', 3,
 ( #28210, #4315, #23701, #17577, #6210, #21518 ),
 .UNSPECIFIED., .F., .F.,
 ( 4, 2, 4 ),
 ( 0.000000000000000000, 0.5000000000000000000, 1.000000000000000000 ),
 .UNSPECIFIED. ) ;
#1085=ORIENTED_EDGE ( 'NONE', *, *, #16389, .T. ) ;
#1148=CARTESIAN_POINT ( 'NONE',  ( -39.83713413880786902, -63.35496135694597086, -2.175426268797550744 ) ) ;
#1158=DIRECTION ( 'NONE',  ( -0.7600087925152557711, -0.5000000000001688649, -0.4151946956541399114 ) ) ;
#1159=EDGE_LOOP ( 'NONE', ( #5660, #9858, #7477, #25278 ) ) ;
#1177=CARTESIAN_POINT ( 'NONE',  ( -41.66730568001332102, -65.09474816372230066, -2.847883582410218661 ) ) ;
#1206=EDGE_LOOP ( 'NONE', ( #19518, #1380, #945, #25945 ) ) ;
#1209=CARTESIAN_POINT ( 'NONE',  ( -41.45000000000000284, -63.07912966450000880, -2.857883832489999776 ) ) ;
#1210=ORIENTED_EDGE ( 'NONE', *, *, #15889, .F. ) ;
#1221=DIRECTION ( 'NONE',  ( 0.000000000000000000, -1.000000000000000000, 0.000000000000000000 ) ) ;
#1231=CARTESIAN_POINT ( 'NONE',  ( -43.29730172082344808, -65.09619745167302085, 0.03908829158085567329 ) ) ;
#1235=CARTESIAN_POINT ( 'NONE',  ( -40.00000000000000000, -94.00000000000000000, 0.000000000000000000 ) ) ;
#1237=CARTESIAN_POINT ( 'NONE',  ( -41.74999999999191402, -63.07120704560062308, -2.719973428251394321 ) ) ;
#1246=DIRECTION ( 'NONE',  ( 0.000000000000000000, 1.000000000000000000, 0.000000000000000000 ) ) ;
#1249=EDGE_CURVE ( 'NONE', #21436, #3079, #22329, .T. ) ;
#1254=ADVANCED_FACE ( 'NONE', ( #18664 ), #27557, .F. ) ;
#1273=CARTESIAN_POINT ( 'NONE',  ( -41.74156629096919602, -63.06504043304209262, 2.752751128773220479 ) ) ;
#1289=CARTESIAN_POINT ( 'NONE',  ( -41.75000000000000000, -65.63577453799999262, 1.587713240270000048 ) ) ;
#1303=CARTESIAN_POINT ( 'NONE',  ( -41.57851898686420355, -65.10052340105812618, -2.886766141929010931 ) ) ;
#1370=EDGE_LOOP ( 'NONE', ( #24888, #4484, #6016, #12627, #6708, #11813, #11488, #135, #2101, #11875, #891, #8626, #18680, #12669, #5294, #11926 ) ) ;
#1371=EDGE_CURVE ( 'NONE', #24292, #7086, #7735, .T. ) ;
#1380=ORIENTED_EDGE ( 'NONE', *, *, #26895, .T. ) ;
#1408=DIRECTION ( 'NONE',  ( 0.8775825618903718706, 0.000000000000000000, 0.4794255386042046152 ) ) ;
#1459=CARTESIAN_POINT ( 'NONE',  ( -38.31827398130649698, -63.05366291735832363, 2.839252009381883823 ) ) ;
#1464=CARTESIAN_POINT ( 'NONE',  ( -40.50000000000000000, -63.00000000000000000, -2.309401076760000393 ) ) ;
#1481=CIRCLE ( 'NONE', #21469, 0.4999999999999985567 ) ;
#1489=EDGE_CURVE ( 'NONE', #21683, #25610, #7372, .T. ) ;
#1511=CARTESIAN_POINT ( 'NONE',  ( -41.48055058678063034, -63.07121106306871638, -2.875522221980898241 ) ) ;
#1524=CARTESIAN_POINT ( 'NONE',  ( -40.50000000000000000, -65.63577453799999262, -2.309401076760000393 ) ) ;
#1534=DIRECTION ( 'NONE',  ( 1.000000000000000000, 0.000000000000000000, 0.000000000000000000 ) ) ;
#1543=CARTESIAN_POINT ( 'NONE',  ( -43.23056608648008137, -63.07120704560069413, 0.1555577424909893314 ) ) ;
#1600=CARTESIAN_POINT ( 'NONE',  ( -41.80254054884269976, -63.35496709430440632, 1.228761571272451780 ) ) ;
#1625=ORIENTED_EDGE ( 'NONE', *, *, #14208, .T. ) ;
#1626=ADVANCED_FACE ( 'NONE', ( #26713 ), #13285, .T. ) ;
#1665=CARTESIAN_POINT ( 'NONE',  ( -39.95446396948431556, -65.74401273904912557, -2.175432824119099884 ) ) ;
#1673=ORIENTED_EDGE ( 'NONE', *, *, #12243, .T. ) ;
#1687=CIRCLE ( 'NONE', #21673, 4.999999999999997335 ) ;
#1721=EDGE_CURVE ( 'NONE', #7623, #8093, #9792, .T. ) ;
#1741=DIRECTION ( 'NONE',  ( 0.000000000000000000, 0.000000000000000000, 1.000000000000000000 ) ) ;
#1747=CARTESIAN_POINT ( 'NONE',  ( -35.61208719050000582, -63.50000000000000000, 2.397127693020000283 ) ) ;
#1763=VERTEX_POINT ( 'NONE', #25404 ) ;
#1791=CARTESIAN_POINT ( 'NONE',  ( -36.87700573890000300, -65.19264941160000149, 0.2176643648599999870 ) ) ;
#1795=B_SPLINE_CURVE_WITH_KNOTS ( 'NONE', 3,
 ( #12986, #4262, #8757, #13282, #28447, #17818, #22047, #8333, #26558, #2097, #21895 ),
 .UNSPECIFIED., .F., .F.,
 ( 4, 2, 1, 2, 2, 4 ),
 ( 0.000000000000000000, 0.2499999999999964473, 0.3750000000000006661, 0.4375000000000029976, 0.5000000000000053291, 1.000000000000000000 ),
 .UNSPECIFIED. ) ;
#1798=CARTESIAN_POINT ( 'NONE',  ( -40.42464116754384662, -65.66731758214605463, -2.269131925652129400 ) ) ;
#1800=TOROIDAL_SURFACE ( 'NONE', #9229, 3.500000000000000000, 0.5000000000000000000 ) ;
#1809=CARTESIAN_POINT ( 'NONE',  ( -38.08919256720000135, -65.74290439030001210, 1.043878858160000034 ) ) ;
#1810=ORIENTED_EDGE ( 'NONE', *, *, #2181, .T. ) ;
#1815=B_SPLINE_CURVE_WITH_KNOTS ( 'NONE', 3,
 ( #16986, #5900, #1148, #14778, #20946, #5489 ),
 .UNSPECIFIED., .F., .F.,
 ( 4, 2, 4 ),
 ( 0.000000000000000000, 0.5000000000000000000, 1.000000000000000000 ),
 .UNSPECIFIED. ) ;
#1825=CARTESIAN_POINT ( 'NONE',  ( -36.79999999999999716, -63.07912966450000880, -0.1732050807570000017 ) ) ;
#1877=CARTESIAN_POINT ( 'NONE',  ( -41.84021856431421327, -65.74136842487146737, 1.169644296513078663 ) ) ;
#1898=CARTESIAN_POINT ( 'NONE',  ( -38.25000000000000000, -65.41419836839999391, 2.121055962339999823 ) ) ;
#1901=VECTOR ( 'NONE', #9739, 1000.000000000000000 ) ;
#1909=ORIENTED_EDGE ( 'NONE', *, *, #3181, .F. ) ;
#1920=CARTESIAN_POINT ( 'NONE',  ( -39.50000000000000000, -65.63577453799999262, 2.309401076760000393 ) ) ;
#1941=FACE_OUTER_BOUND ( 'NONE', #8168, .T. ) ;
#1960=EDGE_CURVE ( 'NONE', #26414, #9396, #2958, .T. ) ;
#1971=CARTESIAN_POINT ( 'NONE',  ( -36.77331348028479852, -65.13491442160928102, 0.1557320299044409329 ) ) ;
#2024=CARTESIAN_POINT ( 'NONE',  ( -41.80262105942959749, -65.72848773093366503, 1.265555823039845151 ) ) ;
#2025=CARTESIAN_POINT ( 'NONE',  ( -42.25000000000000000, -63.30468293320000583, -0.7216878364880000563 ) ) ;
#2048=EDGE_CURVE ( 'NONE', #4023, #14266, #12241, .T. ) ;
#2092=EDGE_CURVE ( 'NONE', #20079, #20678, #14144, .T. ) ;
#2097=CARTESIAN_POINT ( 'NONE',  ( -42.18414812522917146, -65.66527319018285880, -0.7597074341180621859 ) ) ;
#2101=ORIENTED_EDGE ( 'NONE', *, *, #19442, .F. ) ;
#2122=ORIENTED_EDGE ( 'NONE', *, *, #16389, .F. ) ;
#2167=CARTESIAN_POINT ( 'NONE',  ( -43.20000000000000284, -63.07912966450000880, -0.1732050807570000017 ) ) ;
#2181=EDGE_CURVE ( 'NONE', #28363, #1763, #22679, .T. ) ;
#2233=ORIENTED_EDGE ( 'NONE', *, *, #13610, .T. ) ;
#2247=EDGE_CURVE ( 'NONE', #22254, #14956, #14010, .T. ) ;
#2254=CARTESIAN_POINT ( 'NONE',  ( -41.75000000000000000, -65.00000000000000000, -1.587713240270000048 ) ) ;
#2255=CARTESIAN_POINT ( 'NONE',  ( -38.41282619387080643, -65.10053925467562408, -2.881807801408382996 ) ) ;
#2286=CARTESIAN_POINT ( 'NONE',  ( -41.75000000000000000, -65.14977478849999670, 2.684678751729999480 ) ) ;
#2290=DIRECTION ( 'NONE',  ( 0.8775825618903718706, 0.000000000000000000, 0.4794255386042046152 ) ) ;
#2312=EDGE_LOOP ( 'NONE', ( #13806, #16379, #14686, #21407 ) ) ;
#2318=CARTESIAN_POINT ( 'NONE',  ( -41.82037221943573968, -63.35319846926733334, -1.206297397086846690 ) ) ;
#2346=EDGE_CURVE ( 'NONE', #10898, #19704, #19179, .T. ) ;
#2354=VERTEX_POINT ( 'NONE', #4785 ) ;
#2361=LINE ( 'NONE', #11957, #7893 ) ;
#2375=EDGE_LOOP ( 'NONE', ( #4227, #7103, #488 ) ) ;
#2390=EDGE_LOOP ( 'NONE', ( #10843, #12813 ) ) ;
#2415=CARTESIAN_POINT ( 'NONE',  ( -38.25000000000000000, -63.30468293320000583, -1.587713240270000048 ) ) ;
#2426=FACE_OUTER_BOUND ( 'NONE', #21411, .T. ) ;
#2448=PLANE ( 'NONE',  #27941 ) ;
#2466=VECTOR ( 'NONE', #1221, 1000.000000000000000 ) ;
#2494=ORIENTED_EDGE ( 'NONE', *, *, #25919, .T. ) ;
#2508=CARTESIAN_POINT ( 'NONE',  ( -38.25000000000000000, -65.65254685980617921, -1.544478930961744156 ) ) ;
#2510=VERTEX_POINT ( 'NONE', #25751 ) ;
#2534=CARTESIAN_POINT ( 'NONE',  ( -40.50000000000000000, -63.00000000000000000, -2.309401076760000393 ) ) ;
#2554=CARTESIAN_POINT ( 'NONE',  ( -38.55000000000000426, -63.07912966450000880, -2.857883832489999776 ) ) ;
#2575=CARTESIAN_POINT ( 'NONE',  ( -40.50000000000000000, -64.47022873560000278, -2.309401076760000393 ) ) ;
#2582=CARTESIAN_POINT ( 'NONE',  ( -41.08545581620644072, -63.17361819572722936, -2.647414149845592313 ) ) ;
#2583=AXIS2_PLACEMENT_3D ( 'NONE', #11642, #3086, #9466 ) ;
#2585=DIRECTION ( 'NONE',  ( 0.000000000000000000, -1.000000000000000000, 0.000000000000000000 ) ) ;
#2592=FACE_OUTER_BOUND ( 'NONE', #9327, .T. ) ;
#2594=EDGE_CURVE ( 'NONE', #19704, #12283, #3875, .T. ) ;
#2606=LINE ( 'NONE', #26633, #8801 ) ;
#2615=LINE ( 'NONE', #11465, #15190 ) ;
#2643=CARTESIAN_POINT ( 'NONE',  ( -41.75000000000000000, -65.49083508809999898, -1.947031612740000028 ) ) ;
#2661=FACE_OUTER_BOUND ( 'NONE', #16860, .T. ) ;
#2664=EDGE_CURVE ( 'NONE', #24292, #20440, #167, .T. ) ;
#2688=DIRECTION ( 'NONE',  ( 0.000000000000000000, 1.000000000000000000, 0.000000000000000000 ) ) ;
#2694=ADVANCED_FACE ( 'NONE', ( #28490 ), #28347, .T. ) ;
#2695=CARTESIAN_POINT ( 'NONE',  ( -38.08919256720000135, -65.74290439030001210, 1.043878858160000034 ) ) ;
#2697=CARTESIAN_POINT ( 'NONE',  ( -38.25000000000000000, -65.14977478849999670, 2.684678751729999480 ) ) ;
#2706=ADVANCED_FACE ( 'NONE', ( #13029 ), #22227, .T. ) ;
#2739=ADVANCED_FACE ( 'NONE', ( #13184 ), #21790, .T. ) ;
#2743=ORIENTED_EDGE ( 'NONE', *, *, #9045, .F. ) ;
#2744=AXIS2_PLACEMENT_3D ( 'NONE', #18895, #21634, #1408 ) ;
#2801=CARTESIAN_POINT ( 'NONE',  ( -38.22259796004242816, -65.70975255743678645, -1.354924268994119885 ) ) ;
#2814=AXIS2_PLACEMENT_3D ( 'NONE', #3591, #18624, #27928 ) ;
#2817=ORIENTED_EDGE ( 'NONE', *, *, #27726, .F. ) ;
#2822=CARTESIAN_POINT ( 'NONE',  ( -39.50000000000000000, -64.47022873560000278, 2.309401076760000393 ) ) ;
#2833=DIRECTION ( 'NONE',  ( 0.8775825618903724257, 0.000000000000000000, 0.4794255386042036160 ) ) ;
#2835=VERTEX_POINT ( 'NONE', #15208 ) ;
#2869=LINE ( 'NONE', #6796, #25350 ) ;
#2896=ORIENTED_EDGE ( 'NONE', *, *, #18686, .T. ) ;
#2958=CIRCLE ( 'NONE', #12223, 0.4999999999999985567 ) ;
#2980=CARTESIAN_POINT ( 'NONE',  ( -40.87758256189999884, -66.42264973080000345, -0.4794255386039999456 ) ) ;
#2985=CARTESIAN_POINT ( 'NONE',  ( -36.79999999999999716, -65.14977478849999670, 0.1732050807570000017 ) ) ;
#2994=CARTESIAN_POINT ( 'NONE',  ( -38.48840878260216414, -63.06523941402249278, -2.884620168990968292 ) ) ;
#3008=LINE ( 'NONE', #833, #21963 ) ;
#3019=B_SPLINE_CURVE_WITH_KNOTS ( 'NONE', 3,
 ( #6918, #24836, #6473, #10954, #11553, #17696, #26582, #6626, #22359, #15487, #4434, #2255, #11101, #20014, #26739, #6775, #15636, #25555 ),
 .UNSPECIFIED., .F., .F.,
 ( 4, 2, 2, 2, 2, 2, 2, 2, 4 ),
 ( 0.000000000000000000, 0.1249999999999961142, 0.1874999999999941713, 0.2499999999999922284, 0.4999999999999658606, 0.6249999999999715783, 0.6874999999999747979, 0.7499999999999779066, 1.000000000000000000 ),
 .UNSPECIFIED. ) ;
#3045=CARTESIAN_POINT ( 'NONE',  ( -39.50000000000000000, -63.30468293320000583, -2.309401076760000393 ) ) ;
#3076=CARTESIAN_POINT ( 'NONE',  ( -38.62700573890000300, -65.19264941160000149, -2.813424548380000001 ) ) ;
#3079=VERTEX_POINT ( 'NONE', #990 ) ;
#3080=DIRECTION ( 'NONE',  ( 1.000000000000000000, 0.000000000000000000, 0.000000000000000000 ) ) ;
#3086=DIRECTION ( 'NONE',  ( 0.000000000000000000, -1.000000000000000000, 0.000000000000000000 ) ) ;
#3104=CARTESIAN_POINT ( 'NONE',  ( -38.23742073339541037, -63.33368279749979024, -1.408367766111304098 ) ) ;
#3115=ADVANCED_FACE ( 'NONE', ( #2426 ), #10970, .F. ) ;
#3150=CARTESIAN_POINT ( 'NONE',  ( -41.45000000000000284, -65.00000000000000000, -2.857883832489999776 ) ) ;
#3175=CARTESIAN_POINT ( 'NONE',  ( -41.33431406180000067, -65.21397798589998729, 2.791092524920000262 ) ) ;
#3181=EDGE_CURVE ( 'NONE', #2510, #25473, #17769, .T. ) ;
#3251=VECTOR ( 'NONE', #19320, 1000.000000000000000 ) ;
#3263=FILL_AREA_STYLE_COLOUR ( '', #21287 ) ;
#3268=CARTESIAN_POINT ( 'NONE',  ( -43.24908333233128133, -65.12255024416487004, -0.1339731005256810936 ) ) ;
#3296=ORIENTED_EDGE ( 'NONE', *, *, #23338, .F. ) ;
#3317=ADVANCED_FACE ( 'NONE', ( #28179 ), #8212, .T. ) ;
#3318=CARTESIAN_POINT ( 'NONE',  ( -41.75000000000000000, -63.30468293320000583, -1.587713240270000048 ) ) ;
#3332=CYLINDRICAL_SURFACE ( 'NONE', #10191, 0.1999999999999997891 ) ;
#3342=CARTESIAN_POINT ( 'NONE',  ( -41.61565191535785146, -65.09473604208761799, -2.877732256211138928 ) ) ;
#3346=ORIENTED_EDGE ( 'NONE', *, *, #6428, .T. ) ;
#3368=VERTEX_POINT ( 'NONE', #1809 ) ;
#3400=CARTESIAN_POINT ( 'NONE',  ( -43.21399166432318850, -65.14196057591203726, -0.1651269895930678189 ) ) ;
#3516=ORIENTED_EDGE ( 'NONE', *, *, #24133, .T. ) ;
#3528=DIRECTION ( 'NONE',  ( 0.5000000000001900702, 0.000000000000000000, -0.8660254037843290176 ) ) ;
#3591=CARTESIAN_POINT ( 'NONE',  ( -41.75000000000000000, -63.00000000000000000, 1.587713240270000048 ) ) ;
#3593=DIRECTION ( 'NONE',  ( 1.000000000000000000, 0.000000000000000000, 0.000000000000000000 ) ) ;
#3595=EDGE_LOOP ( 'NONE', ( #8104, #18530, #6935, #8680 ) ) ;
#3598=ORIENTED_EDGE ( 'NONE', *, *, #16847, .T. ) ;
#3669=CARTESIAN_POINT ( 'NONE',  ( -40.37009550159991988, -65.68577269143263209, 2.246086790230779062 ) ) ;
#3677=CARTESIAN_POINT ( 'NONE',  ( -41.58198193041125279, -63.05619511567597613, -2.885163282589263911 ) ) ;
#3686=CARTESIAN_POINT ( 'NONE',  ( -37.59243475499999931, -65.56519245710001087, 0.6307174998529999632 ) ) ;
#3696=ADVANCED_FACE ( 'NONE', ( #17169 ), #10866, .T. ) ;
#3733=LINE ( 'NONE', #10534, #18762 ) ;
#3747=ORIENTED_EDGE ( 'NONE', *, *, #13616, .T. ) ;
#3754=CARTESIAN_POINT ( 'NONE',  ( -41.70213186180765774, -65.10053925467518354, -2.815436737016979496 ) ) ;
#3757=ORIENTED_EDGE ( 'NONE', *, *, #7877, .F. ) ;
#3768=CARTESIAN_POINT ( 'NONE',  ( -38.29314300141285088, -63.05597747387252383, 2.814055026004789184 ) ) ;
#3776=DIRECTION ( 'NONE',  ( 0.8775825618903718706, 0.000000000000000000, 0.4794255386042046152 ) ) ;
#3787=CARTESIAN_POINT ( 'NONE',  ( -38.25000000000000000, -65.31510159580000163, -2.337827133090000231 ) ) ;
#3810=CARTESIAN_POINT ( 'NONE',  ( -39.64767024207763768, -65.69391135774336021, 2.235876747186491098 ) ) ;
#3859=AXIS2_PLACEMENT_3D ( 'NONE', #555, #7685, #14076 ) ;
#3862=CARTESIAN_POINT ( 'NONE',  ( -37.25000000000000000, -65.00000000000000000, 1.587713240270000048 ) ) ;
#3875=LINE ( 'NONE', #12189, #14945 ) ;
#3890=ORIENTED_EDGE ( 'NONE', *, *, #7784, .T. ) ;
#3917=DIRECTION ( 'NONE',  ( 0.8775825618903724257, 0.000000000000000000, 0.4794255386042036160 ) ) ;
#3924=CARTESIAN_POINT ( 'NONE',  ( -38.25000000000000000, -65.17124718639999514, -2.640283750789999662 ) ) ;
#3930=CARTESIAN_POINT ( 'NONE',  ( -38.66568593819999933, -65.21397798589998729, 2.791092524920000262 ) ) ;
#3960=CARTESIAN_POINT ( 'NONE',  ( -41.51316926232986049, -63.06504043304238394, -2.884616214739031737 ) ) ;
#4002=CARTESIAN_POINT ( 'NONE',  ( -39.50000000000000000, -63.30468293320000583, 2.309401076760000393 ) ) ;
#4016=CARTESIAN_POINT ( 'NONE',  ( -40.00000000000000000, -94.00000000000000000, 0.000000000000000000 ) ) ;
#4023=VERTEX_POINT ( 'NONE', #24020 ) ;
#4044=CARTESIAN_POINT ( 'NONE',  ( -41.78262379717566688, -65.71460843033148080, 1.333804927987287225 ) ) ;
#4046=AXIS2_PLACEMENT_3D ( 'NONE', #21478, #28178, #1534 ) ;
#4070=ORIENTED_EDGE ( 'NONE', *, *, #15260, .T. ) ;
#4076=CARTESIAN_POINT ( 'NONE',  ( -43.12299426110000411, -65.19264941160000149, -0.2176643648609999926 ) ) ;
#4086=CARTESIAN_POINT ( 'NONE',  ( -39.95292656566140721, -65.74401284883323626, 2.175430544872245964 ) ) ;
#4098=ORIENTED_EDGE ( 'NONE', *, *, #24752, .T. ) ;
#4128=CARTESIAN_POINT ( 'NONE',  ( -43.29047163944868259, -63.05597747387585628, 0.07115400839859020721 ) ) ;
#4155=CARTESIAN_POINT ( 'NONE',  ( -36.90000000000000568, -65.00000000000000000, 2.131628207279999844E-14 ) ) ;
#4156=ORIENTED_EDGE ( 'NONE', *, *, #5146, .F. ) ;
#4157=DIRECTION ( 'NONE',  ( 0.8775825618903719816, 0.000000000000000000, 0.4794255386042042821 ) ) ;
#4208=EDGE_CURVE ( 'NONE', #2510, #7623, #1084, .T. ) ;
#4212=CARTESIAN_POINT ( 'NONE',  ( -38.58844719860000083, -65.17124718639999514, 2.835686332019999867 ) ) ;
#4227=ORIENTED_EDGE ( 'NONE', *, *, #18836, .F. ) ;
#4236=VECTOR ( 'NONE', #21129, 1000.000000000000000 ) ;
#4259=ORIENTED_EDGE ( 'NONE', *, *, #2346, .F. ) ;
#4262=CARTESIAN_POINT ( 'NONE',  ( -41.93357002089393859, -65.74109373451008764, -1.008753740007117816 ) ) ;
#4315=CARTESIAN_POINT ( 'NONE',  ( -40.33877555573290863, -63.33820092556621972, 2.216318100457958629 ) ) ;
#4345=CARTESIAN_POINT ( 'NONE',  ( -41.93083144778949389, -65.74402527487352188, 1.006537937124212911 ) ) ;
#4347=DIRECTION ( 'NONE',  ( 0.000000000000000000, -1.000000000000000000, 0.000000000000000000 ) ) ;
#4369=ADVANCED_FACE ( 'NONE', ( #26712 ), #1800, .F. ) ;
#4383=DIRECTION ( 'NONE',  ( 0.000000000000000000, -1.000000000000000000, 0.000000000000000000 ) ) ;
#4422=DIRECTION ( 'NONE',  ( 0.8775825618903724257, 0.000000000000000000, 0.4794255386042037825 ) ) ;
#4434=CARTESIAN_POINT ( 'NONE',  ( -38.38520059305543697, -65.09619745166223481, -2.875091199968994093 ) ) ;
#4446=EDGE_CURVE ( 'NONE', #28390, #13967, #21186, .T. ) ;
#4484=ORIENTED_EDGE ( 'NONE', *, *, #24003, .T. ) ;
#4487=CARTESIAN_POINT ( 'NONE',  ( -37.75000000000000000, -65.00000000000000000, -0.7216878364849999006 ) ) ;
#4501=CARTESIAN_POINT ( 'NONE',  ( -36.92846103339999786, -63.00000000000000000, 1.677989385109999843 ) ) ;
#4527=FACE_OUTER_BOUND ( 'NONE', #21595, .T. ) ;
#4536=( GEOMETRIC_REPRESENTATION_CONTEXT ( 3 ) GLOBAL_UNCERTAINTY_ASSIGNED_CONTEXT ( ( #16739 ) ) GLOBAL_UNIT_ASSIGNED_CONTEXT ( ( #7496, #18263, #9510 ) ) REPRESENTATION_CONTEXT ( 'NONE', 'WORKASPACE' ) );
#4595=FACE_BOUND ( 'NONE', #12615, .T. ) ;
#4604=DIRECTION ( 'NONE',  ( 0.8775825618903720926, 0.000000000000000000, 0.4794255386042039491 ) ) ;
#4612=CARTESIAN_POINT ( 'NONE',  ( -40.00000000000000000, -94.00000000000000000, 0.000000000000000000 ) ) ;
#4647=CARTESIAN_POINT ( 'NONE',  ( -38.55000000000000426, -65.14977478849999670, 2.857883832489999776 ) ) ;
#4667=ORIENTED_EDGE ( 'NONE', *, *, #12318, .F. ) ;
#4671=DIRECTION ( 'NONE',  ( 0.000000000000000000, -1.000000000000000000, 0.000000000000000000 ) ) ;
#4742=AXIS2_PLACEMENT_3D ( 'NONE', #4016, #26761, #4157 ) ;
#4746=LINE ( 'NONE', #2575, #12542 ) ;
#4760=CARTESIAN_POINT ( 'NONE',  ( -41.45000000000000284, -65.14977478849999670, 2.857883832489999776 ) ) ;
#4771=B_SPLINE_CURVE_WITH_KNOTS ( 'NONE', 3,
 ( #6546, #10881, #26361, #19791 ),
 .UNSPECIFIED., .F., .F.,
 ( 4, 4 ),
 ( 0.000000000000000000, 1.000000000000000000 ),
 .UNSPECIFIED. ) ;
#4785=CARTESIAN_POINT ( 'NONE',  ( -42.63274768570000361, -69.50000000000000000, -1.438276615809999992 ) ) ;
#4829=CARTESIAN_POINT ( 'NONE',  ( -41.75000000000000000, -63.17361819574031045, 2.263739386364747919 ) ) ;
#4832=EDGE_LOOP ( 'NONE', ( #18242, #16244, #22403, #12092 ) ) ;
#4834=CARTESIAN_POINT ( 'NONE',  ( -38.19683097078898015, -65.73348302053989300, -1.252585022352845412 ) ) ;
#4872=CARTESIAN_POINT ( 'NONE',  ( -38.38199864144505113, -63.05366291736240214, -2.876043459049374196 ) ) ;
#4884=CARTESIAN_POINT ( 'NONE',  ( -44.38791280949999418, -63.50000000000000000, -2.397127693020000283 ) ) ;
#4905=DIRECTION ( 'NONE',  ( 0.4794255386042028944, 0.000000000000000000, -0.8775825618903727587 ) ) ;
#4937=B_SPLINE_CURVE_WITH_KNOTS ( 'NONE', 3,
 ( #2025, #17605, #15389, #2167 ),
 .UNSPECIFIED., .F., .F.,
 ( 4, 4 ),
 ( 0.000000000000000000, 1.000000000000000000 ),
 .UNSPECIFIED. ) ;
#4938=CARTESIAN_POINT ( 'NONE',  ( -43.20000000000000284, -65.00000000000000000, -0.1732050807570000017 ) ) ;
#4957=CARTESIAN_POINT ( 'NONE',  ( -41.75000000000000000, -65.31510159580000163, -2.337827133099999788 ) ) ;
#4970=CARTESIAN_POINT ( 'NONE',  ( -37.95315413403665872, -65.71452780515592451, -0.8766092144919545026 ) ) ;
#4982=DIRECTION ( 'NONE',  ( 0.8775825618903720926, 0.000000000000000000, 0.4794255386042039491 ) ) ;
#5054=ORIENTED_EDGE ( 'NONE', *, *, #24540, .T. ) ;
#5061=AXIS2_PLACEMENT_3D ( 'NONE', #14357, #17102, #7940 ) ;
#5143=ORIENTED_EDGE ( 'NONE', *, *, #14512, .F. ) ;
#5146=EDGE_CURVE ( 'NONE', #9249, #21683, #17224, .T. ) ;
#5148=SURFACE_SIDE_STYLE ('',( #25117 ) ) ;
#5167=CARTESIAN_POINT ( 'NONE',  ( -43.20000000000000284, -65.14977478849999670, 0.1732050807559999961 ) ) ;
#5183=ORIENTED_EDGE ( 'NONE', *, *, #18686, .F. ) ;
#5203=CARTESIAN_POINT ( 'NONE',  ( -41.70763373158882814, -63.05619511567403634, 2.812618181363554015 ) ) ;
#5221=ORIENTED_EDGE ( 'NONE', *, *, #11152, .F. ) ;
#5241=EDGE_CURVE ( 'NONE', #1763, #14956, #2361, .T. ) ;
#5249=ADVANCED_FACE ( 'NONE', ( #2661 ), #638, .T. ) ;
#5266=VERTEX_POINT ( 'NONE', #27425 ) ;
#5284=VECTOR ( 'NONE', #20673, 1000.000000000000000 ) ;
#5294=ORIENTED_EDGE ( 'NONE', *, *, #22492, .F. ) ;
#5298=FILL_AREA_STYLE ('',( #3263 ) ) ;
#5304=FACE_OUTER_BOUND ( 'NONE', #22857, .T. ) ;
#5335=CARTESIAN_POINT ( 'NONE',  ( -40.77792552671823501, -63.24690319806511241, 2.469861454416400370 ) ) ;
#5340=CARTESIAN_POINT ( 'NONE',  ( -40.00000000000000000, -65.84529946160000691, 0.000000000000000000 ) ) ;
#5386=CLOSED_SHELL ( 'NONE', ( #22330, #27929, #14692, #26645, #26893, #15039, #8994, #15195, #23394, #21803, #2739, #18801, #25258, #15430, #19, #17805, #6794, #3115, #3696, #2694, #26454, #1254, #3317, #5509, #1626, #16358, #15409, #11675, #26517, #27968, #9481, #8128, #18382, #5249, #27531, #28757, #4369, #7123, #2706, #23496, #24885 ) ) ;
#5400=DIRECTION ( 'NONE',  ( 0.4794255386042028944, 0.000000000000000000, -0.8775825618903727587 ) ) ;
#5421=CARTESIAN_POINT ( 'NONE',  ( -38.20646596253030225, -65.72247384671339887, 1.295796974277947822 ) ) ;
#5425=B_SPLINE_CURVE_WITH_KNOTS ( 'NONE', 5,
 ( #17182, #17328, #6248, #5956, #3787, #19371, #26069, #3924, #12788 ),
 .UNSPECIFIED., .F., .F.,
 ( 6, 3, 6 ),
 ( 0.000000000000000000, 1.237573681340000009, 1.566718891470000097 ),
 .UNSPECIFIED. ) ;
#5440=CARTESIAN_POINT ( 'NONE',  ( -43.28930566789392032, -65.10053925468378111, 0.06637106439163820149 ) ) ;
#5448=FACE_OUTER_BOUND ( 'NONE', #12078, .T. ) ;
#5489=CARTESIAN_POINT ( 'NONE',  ( -40.50000000000000000, -63.30468293320000583, -2.309401076760000393 ) ) ;
#5492=( GEOMETRIC_REPRESENTATION_CONTEXT ( 3 ) GLOBAL_UNCERTAINTY_ASSIGNED_CONTEXT ( ( #25491 ) ) GLOBAL_UNIT_ASSIGNED_CONTEXT ( ( #18542, #22773, #9496 ) ) REPRESENTATION_CONTEXT ( 'NONE', 'WORKASPACE' ) );
#5509=ADVANCED_FACE ( 'NONE', ( #11740 ), #27504, .T. ) ;
#5521=CARTESIAN_POINT ( 'NONE',  ( -41.79927756528118721, -65.72601415636299294, -1.277196024497175175 ) ) ;
#5559=CARTESIAN_POINT ( 'NONE',  ( -38.25000000000000000, -65.63577453799999262, 1.587713240270000048 ) ) ;
#5562=DIRECTION ( 'NONE',  ( 0.000000000000000000, 0.000000000000000000, 1.000000000000000000 ) ) ;
#5567=VERTEX_POINT ( 'NONE', #21087 ) ;
#5570=DIRECTION ( 'NONE',  ( -0.8476796612309128731, -0.2588190451029734884, -0.4630895095199519806 ) ) ;
#5580=CARTESIAN_POINT ( 'NONE',  ( -43.22668651970722209, -65.13491442161374323, -0.1557320299099214655 ) ) ;
#5622=CARTESIAN_POINT ( 'NONE',  ( -41.61800135853595606, -63.05366291736181950, 2.876043459062908259 ) ) ;
#5633=CARTESIAN_POINT ( 'NONE',  ( -44.38791280949999418, -66.25000000000000000, -2.397127693020000283 ) ) ;
#5645=CARTESIAN_POINT ( 'NONE',  ( -40.00000000000000000, -67.00000000000000000, 0.000000000000000000 ) ) ;
#5660=ORIENTED_EDGE ( 'NONE', *, *, #27726, .T. ) ;
#5674=CARTESIAN_POINT ( 'NONE',  ( -41.74999999999813127, -63.33820666349189565, 1.401515418006119118 ) ) ;
#5719=VECTOR ( 'NONE', #23042, 1000.000000000000000 ) ;
#5734=EDGE_CURVE ( 'NONE', #5266, #12283, #3019, .T. ) ;
#5797=CARTESIAN_POINT ( 'NONE',  ( -41.72484683961315000, -65.10974319587182890, -2.782833434445878940 ) ) ;
#5805=EDGE_LOOP ( 'NONE', ( #15435, #17846, #23210, #26823 ) ) ;
#5813=CARTESIAN_POINT ( 'NONE',  ( -42.08877555573144491, -63.33820092556624815, 0.8147708127840216363 ) ) ;
#5826=PLANE ( 'NONE',  #8154 ) ;
#5881=ORIENTED_EDGE ( 'NONE', *, *, #6007, .T. ) ;
#5898=CYLINDRICAL_SURFACE ( 'NONE', #21570, 1.000000000000000888 ) ;
#5900=CARTESIAN_POINT ( 'NONE',  ( -39.66122444415238846, -63.33820092554161363, -2.216318100524186985 ) ) ;
#5901=ORIENTED_EDGE ( 'NONE', *, *, #4208, .F. ) ;
#5925=CARTESIAN_POINT ( 'NONE',  ( -41.50851755762869999, -65.12255024417927984, -2.880775255076511332 ) ) ;
#5926=AXIS2_PLACEMENT_3D ( 'NONE', #18427, #27317, #13755 ) ;
#5940=DIRECTION ( 'NONE',  ( 0.000000000000000000, -1.000000000000000000, 0.000000000000000000 ) ) ;
#5945=VECTOR ( 'NONE', #9955, 1000.000000000000000 ) ;
#5956=CARTESIAN_POINT ( 'NONE',  ( -38.25000000000000000, -65.41419836839999391, -2.121055962329999822 ) ) ;
#6007=EDGE_CURVE ( 'NONE', #17600, #767, #1687, .T. ) ;
#6008=CARTESIAN_POINT ( 'NONE',  ( -40.18318593513492232, -65.73348302056557202, -2.187882697783523955 ) ) ;
#6016=ORIENTED_EDGE ( 'NONE', *, *, #8795, .T. ) ;
#6022=CARTESIAN_POINT ( 'NONE',  ( -43.25473555329831754, -63.06504043304213525, -0.1318650859683790921 ) ) ;
#6035=AXIS2_PLACEMENT_3D ( 'NONE', #23869, #21401, #22223 ) ;
#6075=ORIENTED_EDGE ( 'NONE', *, *, #17561, .T. ) ;
#6082=CARTESIAN_POINT ( 'NONE',  ( -38.25000000000810729, -63.07120704560290392, 2.719973428241237112 ) ) ;
#6087=CARTESIAN_POINT ( 'NONE',  ( -42.25000000000000000, -63.30468293320000583, 0.7216878364880000563 ) ) ;
#6125=CARTESIAN_POINT ( 'NONE',  ( -39.90716760802018115, -65.74136842489099308, 2.178498173436029361 ) ) ;
#6134=CARTESIAN_POINT ( 'NONE',  ( -38.25000000000000000, -63.07912966450000880, -2.684678751729999480 ) ) ;
#6145=CARTESIAN_POINT ( 'NONE',  ( -37.75000000000000000, -65.63577453799999262, 0.7216878364859999895 ) ) ;
#6196=AXIS2_PLACEMENT_3D ( 'NONE', #1235, #27743, #23507 ) ;
#6201=CARTESIAN_POINT ( 'NONE',  ( -37.75000000000000000, -63.00000000000000000, 0.7216878364859999895 ) ) ;
#6202=ORIENTED_EDGE ( 'NONE', *, *, #7160, .T. ) ;
#6210=CARTESIAN_POINT ( 'NONE',  ( -39.66125204418437278, -63.33820666349190986, 2.216302165637858312 ) ) ;
#6233=CARTESIAN_POINT ( 'NONE',  ( -42.08349140526518539, -65.70258710782505318, 0.8420150274644456756 ) ) ;
#6248=CARTESIAN_POINT ( 'NONE',  ( -38.25000000000000000, -65.49083508809999898, -1.947031612740000028 ) ) ;
#6279=ORIENTED_EDGE ( 'NONE', *, *, #26164, .F. ) ;
#6284=EDGE_LOOP ( 'NONE', ( #10363, #5054, #20349, #5143 ) ) ;
#6291=ORIENTED_EDGE ( 'NONE', *, *, #8795, .F. ) ;
#6297=CARTESIAN_POINT ( 'NONE',  ( -39.84007938994317044, -65.73345158628970353, -2.188026723677208629 ) ) ;
#6320=CARTESIAN_POINT ( 'NONE',  ( -43.10000000000000142, -65.00000000000000000, -4.511807594199999947E-13 ) ) ;
#6329=ORIENTED_EDGE ( 'NONE', *, *, #24003, .F. ) ;
#6371=CARTESIAN_POINT ( 'NONE',  ( -42.13021597025726095, -65.68577269143236208, 0.8025312888707835102 ) ) ;
#6382=CARTESIAN_POINT ( 'NONE',  ( -42.63274768570000361, -94.00000000000000000, -1.438276615809999992 ) ) ;
#6386=AXIS2_PLACEMENT_3D ( 'NONE', #16524, #11701, #14336 ) ;
#6394=CARTESIAN_POINT ( 'NONE',  ( -39.03811165380000148, -65.41419836839999391, 2.576072437790000169 ) ) ;
#6402=CARTESIAN_POINT ( 'NONE',  ( -42.25000000000000000, -65.63577453799999262, -0.7216878364880000563 ) ) ;
#6427=CARTESIAN_POINT ( 'NONE',  ( -38.25000000000000000, -65.00000000000000000, -2.684678751729999480 ) ) ;
#6428=EDGE_CURVE ( 'NONE', #8977, #17600, #9817, .T. ) ;
#6438=ORIENTED_EDGE ( 'NONE', *, *, #7784, .F. ) ;
#6440=TOROIDAL_SURFACE ( 'NONE', #22761, 3.500000000000000000, 0.5000000000000000000 ) ;
#6447=DIRECTION ( 'NONE',  ( -0.8660254037838959196, 0.000000000000000000, 0.5000000000009399148 ) ) ;
#6466=CARTESIAN_POINT ( 'NONE',  ( -36.77200237156692708, -65.13413837703032527, -0.1570406424484263597 ) ) ;
#6473=CARTESIAN_POINT ( 'NONE',  ( -38.25178884604896723, -65.13491442161021894, -2.716526481159466488 ) ) ;
#6476=VERTEX_POINT ( 'NONE', #14210 ) ;
#6498=CARTESIAN_POINT ( 'NONE',  ( -42.41335204520000701, -63.20096189429999356, -1.318420231159999956 ) ) ;
#6523=CARTESIAN_POINT ( 'NONE',  ( -41.45000000000000284, -65.14977478849999670, 2.857883832489999776 ) ) ;
#6528=ORIENTED_EDGE ( 'NONE', *, *, #26610, .T. ) ;
#6530=CARTESIAN_POINT ( 'NONE',  ( -41.79245735104326087, -65.72204893722175711, 1.298727208254003784 ) ) ;
#6534=DIRECTION ( 'NONE',  ( -0.5000000000001900702, 0.000000000000000000, 0.8660254037843290176 ) ) ;
#6546=CARTESIAN_POINT ( 'NONE',  ( -38.25000000000000000, -63.30468293320000583, 1.587713240270000048 ) ) ;
#6575=CARTESIAN_POINT ( 'NONE',  ( -38.55000000000000426, -65.00000000000000000, 2.857883832489999776 ) ) ;
#6598=VERTEX_POINT ( 'NONE', #24853 ) ;
#6616=CARTESIAN_POINT ( 'NONE',  ( -43.23055058677169171, -63.07121106306891534, -0.1555666912528072821 ) ) ;
#6626=CARTESIAN_POINT ( 'NONE',  ( -38.28924667970461826, -65.10052340105359292, -2.810420613934208944 ) ) ;
#6679=CARTESIAN_POINT ( 'NONE',  ( -42.21358016755470288, -65.65208897057404158, 0.7427148365544418152 ) ) ;
#6682=LINE ( 'NONE', #4487, #10838 ) ;
#6696=CARTESIAN_POINT ( 'NONE',  ( -38.25000000000000000, -65.14977478849999670, 2.684678751729999480 ) ) ;
#6708=ORIENTED_EDGE ( 'NONE', *, *, #16774, .T. ) ;
#6731=ORIENTED_EDGE ( 'NONE', *, *, #9124, .F. ) ;
#6747=VECTOR ( 'NONE', #16235, 1000.000000000000000 ) ;
#6765=B_SPLINE_CURVE_WITH_KNOTS ( 'NONE', 3,
 ( #27064, #24283, #20205, #7108 ),
 .UNSPECIFIED., .F., .F.,
 ( 4, 4 ),
 ( 0.000000000000000000, 1.000000000000000000 ),
 .UNSPECIFIED. ) ;
#6769=EDGE_LOOP ( 'NONE', ( #19257, #1673, #19762, #12759 ) ) ;
#6775=CARTESIAN_POINT ( 'NONE',  ( -38.49205360668217679, -65.12158389261927027, -2.883084786666632482 ) ) ;
#6794=ADVANCED_FACE ( 'NONE', ( #24080 ), #10795, .T. ) ;
#6796=CARTESIAN_POINT ( 'NONE',  ( -37.36725231429999639, -81.75000000000000000, 1.438276615809999992 ) ) ;
#6803=CARTESIAN_POINT ( 'NONE',  ( -41.51571301719197038, -65.11307468787710206, 2.895823260651953834 ) ) ;
#6825=ORIENTED_EDGE ( 'NONE', *, *, #18279, .T. ) ;
#6826=CARTESIAN_POINT ( 'NONE',  ( -38.90721607023505157, -63.17171877516572209, -2.651645038172750102 ) ) ;
#6858=DIRECTION ( 'NONE',  ( 1.000000000000000000, 0.000000000000000000, 0.000000000000000000 ) ) ;
#6869=DIRECTION ( 'NONE',  ( 0.000000000000000000, -1.000000000000000000, 0.000000000000000000 ) ) ;
#6872=VERTEX_POINT ( 'NONE', #10937 ) ;
#6917=LINE ( 'NONE', #2254, #27986 ) ;
#6918=CARTESIAN_POINT ( 'NONE',  ( -38.25000000000000000, -65.14977478849999670, -2.684678751729999480 ) ) ;
#6935=ORIENTED_EDGE ( 'NONE', *, *, #24540, .F. ) ;
#6938=CARTESIAN_POINT ( 'NONE',  ( -41.09278392978337990, -63.17171877516095435, 2.651645038183386482 ) ) ;
#6939=ORIENTED_EDGE ( 'NONE', *, *, #20230, .T. ) ;
#7027=DIRECTION ( 'NONE',  ( 0.000000000000000000, -1.000000000000000000, 0.000000000000000000 ) ) ;
#7056=CARTESIAN_POINT ( 'NONE',  ( -36.91568593819999933, -65.21397798589998729, -0.2399963883289999989 ) ) ;
#7062=EDGE_CURVE ( 'NONE', #14956, #24995, #7449, .T. ) ;
#7086=VERTEX_POINT ( 'NONE', #5645 ) ;
#7103=ORIENTED_EDGE ( 'NONE', *, *, #15393, .T. ) ;
#7108=CARTESIAN_POINT ( 'NONE',  ( -36.79999999999999716, -63.07912966450000880, 0.1732050807570000017 ) ) ;
#7111=FACE_OUTER_BOUND ( 'NONE', #23761, .T. ) ;
#7123=ADVANCED_FACE ( 'NONE', ( #10942 ), #6440, .F. ) ;
#7143=CARTESIAN_POINT ( 'NONE',  ( -38.55000000000000426, -65.14977478849999670, -2.857883832489999776 ) ) ;
#7160=EDGE_CURVE ( 'NONE', #17027, #14123, #8789, .T. ) ;
#7170=CARTESIAN_POINT ( 'NONE',  ( -38.00285745627953560, -65.72850285332773979, -0.9288085058657069570 ) ) ;
#7208=CARTESIAN_POINT ( 'NONE',  ( -37.93569409864744557, -65.70894154424837552, 0.8597713696862059329 ) ) ;
#7248=CARTESIAN_POINT ( 'NONE',  ( -41.45000000000000284, -63.07912966450000880, 2.857883832489999776 ) ) ;
#7255=CIRCLE ( 'NONE', #26313, 3.500000000000003109 ) ;
#7271=ORIENTED_EDGE ( 'NONE', *, *, #8341, .T. ) ;
#7329=EDGE_CURVE ( 'NONE', #18068, #8093, #17848, .T. ) ;
#7355=CARTESIAN_POINT ( 'NONE',  ( -38.41638535914064079, -63.05597747387668761, -2.885209034396270411 ) ) ;
#7372=LINE ( 'NONE', #3150, #6747 ) ;
#7401=EDGE_LOOP ( 'NONE', ( #15209, #21676, #492, #14588 ) ) ;
#7449=B_SPLINE_CURVE_WITH_KNOTS ( 'NONE', 5,
 ( #1289, #10132, #19848, #8629, #17682, #19052, #7837, #25614, #10654 ),
 .UNSPECIFIED., .F., .F.,
 ( 6, 3, 6 ),
 ( 0.000000000000000000, 1.237573681320000007, 1.566718891449999873 ),
 .UNSPECIFIED. ) ;
#7455=ORIENTED_EDGE ( 'NONE', *, *, #8070, .T. ) ;
#7459=CARTESIAN_POINT ( 'NONE',  ( -37.75000000000000000, -63.30468293320000583, -0.7216878364849999006 ) ) ;
#7466=CARTESIAN_POINT ( 'NONE',  ( -40.81117883860000006, -65.49083508809999898, -2.489060262989999828 ) ) ;
#7476=DIRECTION ( 'NONE',  ( 0.5000000000001886269, 0.000000000000000000, 0.8660254037843296837 ) ) ;
#7477=ORIENTED_EDGE ( 'NONE', *, *, #8070, .F. ) ;
#7496=( LENGTH_UNIT ( ) NAMED_UNIT ( * ) SI_UNIT ( .MILLI., .METRE. ) );
#7503=CARTESIAN_POINT ( 'NONE',  ( -43.24373363001436132, -65.12549727759811447, -0.1396600726280878280 ) ) ;
#7524=VECTOR ( 'NONE', #18174, 1000.000000000000000 ) ;
#7566=FACE_OUTER_BOUND ( 'NONE', #6284, .T. ) ;
#7588=CARTESIAN_POINT ( 'NONE',  ( -41.74285146984968975, -65.12158389260652314, -2.747462277523349705 ) ) ;
#7589=CARTESIAN_POINT ( 'NONE',  ( -38.66568593819999933, -65.21397798589998729, -2.791092524920000262 ) ) ;
#7623=VERTEX_POINT ( 'NONE', #12916 ) ;
#7628=CARTESIAN_POINT ( 'NONE',  ( -38.21231771845751268, -65.71847493511126004, 1.315734964525751671 ) ) ;
#7637=CARTESIAN_POINT ( 'NONE',  ( -38.51944941322620508, -63.07121106307049274, 2.875522221976945403 ) ) ;
#7658=FACE_OUTER_BOUND ( 'NONE', #25367, .T. ) ;
#7685=DIRECTION ( 'NONE',  ( 0.000000000000000000, -1.000000000000000000, 0.000000000000000000 ) ) ;
#7696=ORIENTED_EDGE ( 'NONE', *, *, #11528, .F. ) ;
#7707=ORIENTED_EDGE ( 'NONE', *, *, #23738, .F. ) ;
#7721=DIRECTION ( 'NONE',  ( 1.000000000000000000, 0.000000000000000000, 0.000000000000000000 ) ) ;
#7735=LINE ( 'NONE', #25780, #19764 ) ;
#7762=CARTESIAN_POINT ( 'NONE',  ( -38.21017963042245214, -65.72001381778288476, 1.308254260898115140 ) ) ;
#7771=CARTESIAN_POINT ( 'NONE',  ( -38.25000000000000000, -63.07912966450000880, -2.684678751729999480 ) ) ;
#7784=EDGE_CURVE ( 'NONE', #10898, #6598, #2615, .T. ) ;
#7837=CARTESIAN_POINT ( 'NONE',  ( -41.75000000000000000, -65.19264941160000149, 2.595760183509999930 ) ) ;
#7877=EDGE_CURVE ( 'NONE', #9232, #9396, #22398, .T. ) ;
#7893=VECTOR ( 'NONE', #7027, 1000.000000000000000 ) ;
#7921=AXIS2_PLACEMENT_3D ( 'NONE', #136, #25028, #11603 ) ;
#7940=DIRECTION ( 'NONE',  ( 0.000000000000000000, -1.000000000000000000, 0.000000000000000000 ) ) ;
#7954=CARTESIAN_POINT ( 'NONE',  ( -41.45000000000000284, -63.07912966450000880, 2.857883832489999776 ) ) ;
#7958=CARTESIAN_POINT ( 'NONE',  ( -41.37299426109999700, -65.19264941160000149, 2.813424548390000002 ) ) ;
#7959=VECTOR ( 'NONE', #2688, 1000.000000000000000 ) ;
#7967=DIRECTION ( 'NONE',  ( 1.000000000000000000, 0.000000000000000000, 0.000000000000000000 ) ) ;
#7982=DIRECTION ( 'NONE',  ( 1.000000000000000000, 0.000000000000000000, 0.000000000000000000 ) ) ;
#7983=CARTESIAN_POINT ( 'NONE',  ( -40.00000000000000000, -94.00000000000000000, 0.000000000000000000 ) ) ;
#7987=CARTESIAN_POINT ( 'NONE',  ( -37.75000000000000000, -64.47022873560000278, 0.7216878364859999895 ) ) ;
#8026=AXIS2_PLACEMENT_3D ( 'NONE', #4155, #12873, #24266 ) ;
#8057=EDGE_LOOP ( 'NONE', ( #21977, #24714, #6438, #28620 ) ) ;
#8063=DIRECTION ( 'NONE',  ( 0.000000000000000000, -1.000000000000000000, 0.000000000000000000 ) ) ;
#8070=EDGE_CURVE ( 'NONE', #9249, #3079, #22232, .T. ) ;
#8092=DIRECTION ( 'NONE',  ( 0.7600087925152557711, 0.5000000000001688649, 0.4151946956541399114 ) ) ;
#8093=VERTEX_POINT ( 'NONE', #24273 ) ;
#8104=ORIENTED_EDGE ( 'NONE', *, *, #23213, .T. ) ;
#8124=CARTESIAN_POINT ( 'NONE',  ( -41.68250231393139416, -65.09619745166486382, -2.836002908389325672 ) ) ;
#8128=ADVANCED_FACE ( 'NONE', ( #27052 ), #12066, .T. ) ;
#8154=AXIS2_PLACEMENT_3D ( 'NONE', #17040, #26218, #1741 ) ;
#8157=ORIENTED_EDGE ( 'NONE', *, *, #24133, .F. ) ;
#8168=EDGE_LOOP ( 'NONE', ( #4070, #15592 ) ) ;
#8179=CARTESIAN_POINT ( 'NONE',  ( -39.74894630217540481, -65.71742637285102262, 2.207278035994531429 ) ) ;
#8209=DIRECTION ( 'NONE',  ( -0.5000000000009400258, 0.000000000000000000, -0.8660254037838960306 ) ) ;
#8212=PLANE ( 'NONE',  #5061 ) ;
#8265=CARTESIAN_POINT ( 'NONE',  ( -38.38202296894133525, -63.05366661936223949, 2.876041293754835859 ) ) ;
#8294=EDGE_LOOP ( 'NONE', ( #9467, #16781, #23269, #25085 ) ) ;
#8314=DIRECTION ( 'NONE',  ( 0.8775825618903719816, 0.000000000000000000, 0.4794255386042042821 ) ) ;
#8333=CARTESIAN_POINT ( 'NONE',  ( -42.06430546961426842, -65.70894168417346748, -0.8597717761772040168 ) ) ;
#8341=EDGE_CURVE ( 'NONE', #21937, #767, #25744, .T. ) ;
#8359=ORIENTED_EDGE ( 'NONE', *, *, #16774, .F. ) ;
#8361=ORIENTED_EDGE ( 'NONE', *, *, #23213, .F. ) ;
#8428=CARTESIAN_POINT ( 'NONE',  ( -38.25000000000000000, -63.07912966450000880, 2.684678751729999480 ) ) ;
#8450=CARTESIAN_POINT ( 'NONE',  ( -43.20000000000000284, -63.07912966450000880, -0.1732050807570000017 ) ) ;
#8461=CARTESIAN_POINT ( 'NONE',  ( -41.75000000000000000, -63.07912966450000880, -2.684678751739999925 ) ) ;
#8480=CARTESIAN_POINT ( 'NONE',  ( -40.33934347143421917, -65.69529750894407982, -2.234392387587928575 ) ) ;
#8488=ORIENTED_EDGE ( 'NONE', *, *, #20230, .F. ) ;
#8499=CARTESIAN_POINT ( 'NONE',  ( -43.25394995532027309, -63.06523941402085143, 0.1332336900920622347 ) ) ;
#8504=CARTESIAN_POINT ( 'NONE',  ( -36.75626636997765928, -65.12549727759366647, 0.1396600726223675148 ) ) ;
#8548=B_SPLINE_CURVE_WITH_KNOTS ( 'NONE', 3,
 ( #24242, #1543, #8499, #4128, #28462, #22063, #19852, #6022, #6616, #28735 ),
 .UNSPECIFIED., .F., .F.,
 ( 4, 2, 2, 2, 4 ),
 ( 0.000000000000000000, 0.2500000000000000555, 0.5000000000000000000, 0.7500000000000000000, 1.000000000000000000 ),
 .UNSPECIFIED. ) ;
#8557=CARTESIAN_POINT ( 'NONE',  ( -41.81440164397810122, -65.73344136606142740, 1.233272860631304590 ) ) ;
#8598=CARTESIAN_POINT ( 'NONE',  ( -40.18309971205388109, -65.73347097105947512, 2.187748804568729888 ) ) ;
#8617=DIRECTION ( 'NONE',  ( 0.000000000000000000, 0.000000000000000000, -1.000000000000000000 ) ) ;
#8626=ORIENTED_EDGE ( 'NONE', *, *, #18614, .T. ) ;
#8629=CARTESIAN_POINT ( 'NONE',  ( -41.75000000000000000, -65.41419836839999391, 2.121055962329999822 ) ) ;
#8642=CARTESIAN_POINT ( 'NONE',  ( -36.74920213680079684, -65.12158389260717684, -0.1356225091308175534 ) ) ;
#8680=ORIENTED_EDGE ( 'NONE', *, *, #17561, .F. ) ;
#8686=CARTESIAN_POINT ( 'NONE',  ( -41.75000000000000000, -65.63577453799999262, 1.587713240270000048 ) ) ;
#8689=STYLED_ITEM ( 'NONE', ( #21172 ), #16071 ) ;
#8739=CARTESIAN_POINT ( 'NONE',  ( -38.25000000000000000, -63.30468293320000583, -1.587713240270000048 ) ) ;
#8757=CARTESIAN_POINT ( 'NONE',  ( -41.95806561253180433, -65.73717277034926099, -0.9755888848881901776 ) ) ;
#8780=CARTESIAN_POINT ( 'NONE',  ( -36.79999999999999716, -65.14977478849999670, 0.1732050807570000017 ) ) ;
#8789=B_SPLINE_CURVE_WITH_KNOTS ( 'NONE', 5,
 ( #18119, #72, #8918, #17828, #24967, #7056, #9209, #24523, #27161 ),
 .UNSPECIFIED., .F., .F.,
 ( 6, 3, 6 ),
 ( 0.000000000000000000, 1.237573681330000008, 1.566718891470000097 ),
 .UNSPECIFIED. ) ;
#8795=EDGE_CURVE ( 'NONE', #22471, #6872, #1795, .T. ) ;
#8799=DIRECTION ( 'NONE',  ( 0.000000000000000000, -1.000000000000000000, 0.000000000000000000 ) ) ;
#8801=VECTOR ( 'NONE', #11314, 1000.000000000000000 ) ;
#8877=CARTESIAN_POINT ( 'NONE',  ( -41.75000000000000000, -63.24880261864031183, 1.898084215881414627 ) ) ;
#8898=DIRECTION ( 'NONE',  ( 0.000000000000000000, -1.000000000000000000, 0.000000000000000000 ) ) ;
#8918=CARTESIAN_POINT ( 'NONE',  ( -37.43882116139999994, -65.49083508809999898, -0.5420286502509998883 ) ) ;
#8943=AXIS2_PLACEMENT_3D ( 'NONE', #2534, #13432, #356 ) ;
#8977=VERTEX_POINT ( 'NONE', #23488 ) ;
#8994=ADVANCED_FACE ( 'NONE', ( #25262 ), #10061, .T. ) ;
#9041=CARTESIAN_POINT ( 'NONE',  ( -37.82842046529857072, -63.32098627082129383, -0.7669639132331649289 ) ) ;
#9045=EDGE_CURVE ( 'NONE', #17502, #28438, #16637, .T. ) ;
#9056=CARTESIAN_POINT ( 'NONE',  ( -42.71188834620000563, -65.41419836839999391, 0.4550164754559999913 ) ) ;
#9073=CARTESIAN_POINT ( 'NONE',  ( -36.70027262279481306, -63.05366291736164186, -0.03679144966704090552 ) ) ;
#9124=EDGE_CURVE ( 'NONE', #6872, #10217, #933, .T. ) ;
#9191=DIRECTION ( 'NONE',  ( 0.000000000000000000, 1.000000000000000000, 0.000000000000000000 ) ) ;
#9198=CARTESIAN_POINT ( 'NONE',  ( -42.89961768690000099, -65.31510159580000163, 0.3466308900760000089 ) ) ;
#9209=CARTESIAN_POINT ( 'NONE',  ( -36.87700573890000300, -65.19264941160000149, -0.2176643648609999926 ) ) ;
#9212=CARTESIAN_POINT ( 'NONE',  ( -36.70952836055239032, -63.05597747387601970, -0.07115400841154578826 ) ) ;
#9220=CARTESIAN_POINT ( 'NONE',  ( -38.25843370903133689, -63.06504043303794305, -2.752751128791679491 ) ) ;
#9228=CIRCLE ( 'NONE', #12926, 4.499999999999997335 ) ;
#9229=AXIS2_PLACEMENT_3D ( 'NONE', #18409, #24515, #16201 ) ;
#9232=VERTEX_POINT ( 'NONE', #25948 ) ;
#9236=B_SPLINE_CURVE_WITH_KNOTS ( 'NONE', 3,
 ( #14189, #3400, #5580, #7503, #3268, #25410, #25542, #20896, #12268, #27455, #1231, #5440, #23357, #20755, #21177, #11692, #664, #18561 ),
 .UNSPECIFIED., .F., .F.,
 ( 4, 2, 2, 2, 2, 2, 2, 2, 4 ),
 ( 0.000000000000000000, 0.1249999999999764633, 0.1874999999999647504, 0.2499999999999531486, 0.4999999999999553690, 0.6249999999999564793, 0.6874999999999633626, 0.7499999999999702460, 1.000000000000000000 ),
 .UNSPECIFIED. ) ;
#9249=VERTEX_POINT ( 'NONE', #17784 ) ;
#9253=B_SPLINE_CURVE_WITH_KNOTS ( 'NONE', 3,
 ( #13559, #2508, #9329, #27130, #11363, #15890, #24797, #2801, #4834, #13712, #11509, #20416, #18234, #7170, #16036, #24941, #4970, #13856, #11655, #18952 ),
 .UNSPECIFIED., .F., .F.,
 ( 4, 2, 1, 2, 2, 2, 2, 1, 2, 2, 4 ),
 ( 0.000000000000000000, 0.1249999999999999722, 0.1874999999999996669, 0.2187500000000030254, 0.2500000000000064393, 0.5000000000000230926, 0.6250000000000311973, 0.6875000000000350830, 0.7187500000000430767, 0.7500000000000509592, 1.000000000000000000 ),
 .UNSPECIFIED. ) ;
#9269=AXIS2_PLACEMENT_3D ( 'NONE', #7983, #23569, #18240 ) ;
#9270=DIRECTION ( 'NONE',  ( -1.000000000000000000, 0.000000000000000000, 0.000000000000000000 ) ) ;
#9306=ORIENTED_EDGE ( 'NONE', *, *, #20238, .T. ) ;
#9308=DIRECTION ( 'NONE',  ( 0.000000000000000000, -1.000000000000000000, 0.000000000000000000 ) ) ;
#9321=CARTESIAN_POINT ( 'NONE',  ( -36.79999999999999716, -65.00000000000000000, 0.1732050807570000017 ) ) ;
#9325=CARTESIAN_POINT ( 'NONE',  ( -41.33431406180000067, -65.21397798589998729, -2.791092524920000262 ) ) ;
#9327=EDGE_LOOP ( 'NONE', ( #11134, #7271, #28043, #24591 ) ) ;
#9329=CARTESIAN_POINT ( 'NONE',  ( -38.24719469161180285, -65.66731758217252946, -1.502316001359380149 ) ) ;
#9381=ORIENTED_EDGE ( 'NONE', *, *, #28617, .T. ) ;
#9396=VERTEX_POINT ( 'NONE', #26825 ) ;
#9448=EDGE_CURVE ( 'NONE', #6476, #14702, #13493, .T. ) ;
#9466=DIRECTION ( 'NONE',  ( -0.5000000000001886269, 0.000000000000000000, -0.8660254037843296837 ) ) ;
#9467=ORIENTED_EDGE ( 'NONE', *, *, #25606, .F. ) ;
#9481=ADVANCED_FACE ( 'NONE', ( #4595, #11118 ), #26899, .F. ) ;
#9496=( NAMED_UNIT ( * ) SI_UNIT ( $, .STERADIAN. ) SOLID_ANGLE_UNIT ( ) );
#9510=( NAMED_UNIT ( * ) SI_UNIT ( $, .STERADIAN. ) SOLID_ANGLE_UNIT ( ) );
#9517=CARTESIAN_POINT ( 'NONE',  ( -36.76944941322930305, -63.07121106306917824, 0.1555666912533766322 ) ) ;
#9530=EDGE_LOOP ( 'NONE', ( #718, #21383, #10627, #8361, #23139, #28343 ) ) ;
#9568=ORIENTED_EDGE ( 'NONE', *, *, #2346, .T. ) ;
#9587=ORIENTED_EDGE ( 'NONE', *, *, #9448, .F. ) ;
#9592=ORIENTED_EDGE ( 'NONE', *, *, #4446, .T. ) ;
#9611=CARTESIAN_POINT ( 'NONE',  ( -41.75000000000000000, -65.56519245710001087, -1.769653913539999790 ) ) ;
#9664=CARTESIAN_POINT ( 'NONE',  ( -38.29236626841033342, -63.05619511568021096, -2.812618181335909462 ) ) ;
#9714=FACE_OUTER_BOUND ( 'NONE', #1159, .T. ) ;
#9731=CARTESIAN_POINT ( 'NONE',  ( -40.00000000000000000, -63.00000000000000000, 0.000000000000000000 ) ) ;
#9739=DIRECTION ( 'NONE',  ( 0.000000000000000000, -1.000000000000000000, 0.000000000000000000 ) ) ;
#9740=CARTESIAN_POINT ( 'NONE',  ( -39.34243475499999221, -65.56519245710001087, -2.400371413390000264 ) ) ;
#9777=DIRECTION ( 'NONE',  ( 1.000000000000000000, 0.000000000000000000, 0.000000000000000000 ) ) ;
#9784=B_SPLINE_CURVE_WITH_KNOTS ( 'NONE', 3,
 ( #13551, #8877, #4829, #11204 ),
 .UNSPECIFIED., .F., .F.,
 ( 4, 4 ),
 ( 0.000000000000000000, 1.000000000000000000 ),
 .UNSPECIFIED. ) ;
#9792=LINE ( 'NONE', #2822, #2466 ) ;
#9817=LINE ( 'NONE', #25429, #12653 ) ;
#9831=VERTEX_POINT ( 'NONE', #7771 ) ;
#9858=ORIENTED_EDGE ( 'NONE', *, *, #1249, .T. ) ;
#9860=CYLINDRICAL_SURFACE ( 'NONE', #11143, 0.1999999999999987899 ) ;
#9871=CARTESIAN_POINT ( 'NONE',  ( -41.75000000000000000, -65.63577453799999262, 1.587713240270000048 ) ) ;
#9890=ORIENTED_EDGE ( 'NONE', *, *, #25014, .T. ) ;
#9897=DIRECTION ( 'NONE',  ( 0.8775825618903718706, 0.000000000000000000, 0.4794255386042046152 ) ) ;
#9909=CARTESIAN_POINT ( 'NONE',  ( -41.75000000000000000, -65.00000000000000000, 2.684678751729999480 ) ) ;
#9918=DIRECTION ( 'NONE',  ( 0.000000000000000000, -1.000000000000000000, 0.000000000000000000 ) ) ;
#9922=CARTESIAN_POINT ( 'NONE',  ( -41.75000000000000000, -63.07912966450000880, 2.684678751729999480 ) ) ;
#9952=CARTESIAN_POINT ( 'NONE',  ( -40.50000000000000000, -65.63577453799999262, 2.309401076760000393 ) ) ;
#9955=DIRECTION ( 'NONE',  ( 0.000000000000000000, -1.000000000000000000, 0.000000000000000000 ) ) ;
#9985=CARTESIAN_POINT ( 'NONE',  ( -41.68173630718685274, -63.05366661935899231, 2.839229858532883455 ) ) ;
#10016=CARTESIAN_POINT ( 'NONE',  ( -41.75000000001212896, -65.13413837703322429, -2.717007628343222958 ) ) ;
#10017=CARTESIAN_POINT ( 'NONE',  ( -41.82835010422233069, -65.73761215452407214, -1.198860239817544748 ) ) ;
#10057=ORIENTED_EDGE ( 'NONE', *, *, #13066, .T. ) ;
#10061=PLANE ( 'NONE',  #18636 ) ;
#10109=EDGE_CURVE ( 'NONE', #767, #17600, #20499, .T. ) ;
#10112=CARTESIAN_POINT ( 'NONE',  ( -41.48056608648862920, -63.07120704560056623, 2.875531170741493447 ) ) ;
#10126=DIRECTION ( 'NONE',  ( 0.000000000000000000, -1.000000000000000000, 0.000000000000000000 ) ) ;
#10128=CARTESIAN_POINT ( 'NONE',  ( -40.00000000000000000, -65.84529946160000691, 0.000000000000000000 ) ) ;
#10132=CARTESIAN_POINT ( 'NONE',  ( -41.75000000000000000, -65.56519245710001087, 1.769653913539999790 ) ) ;
#10140=ORIENTED_EDGE ( 'NONE', *, *, #25606, .T. ) ;
#10148=CARTESIAN_POINT ( 'NONE',  ( -41.91080735079999897, -65.74290444429999525, -1.043878813350000101 ) ) ;
#10191=AXIS2_PLACEMENT_3D ( 'NONE', #6320, #22066, #19857 ) ;
#10213=DIRECTION ( 'NONE',  ( 0.5000000000001884048, 0.000000000000000000, -0.8660254037843300168 ) ) ;
#10217=VERTEX_POINT ( 'NONE', #28519 ) ;
#10259=CARTESIAN_POINT ( 'NONE',  ( -41.14961768690000099, -65.31510159580000163, 2.684458023169999930 ) ) ;
#10278=FACE_OUTER_BOUND ( 'NONE', #26904, .T. ) ;
#10300=CARTESIAN_POINT ( 'NONE',  ( -38.48683073767716678, -63.06504043304416030, 2.884616214735281847 ) ) ;
#10306=CARTESIAN_POINT ( 'NONE',  ( -42.84278392979705785, -63.17171877515596634, 0.3794438750353775203 ) ) ;
#10363=ORIENTED_EDGE ( 'NONE', *, *, #4446, .F. ) ;
#10368=CARTESIAN_POINT ( 'NONE',  ( -40.46255798985529140, -65.65254685978855775, -2.287783922119399183 ) ) ;
#10381=ORIENTED_EDGE ( 'NONE', *, *, #27519, .F. ) ;
#10394=FACE_OUTER_BOUND ( 'NONE', #9530, .T. ) ;
#10407=EDGE_CURVE ( 'NONE', #7623, #13967, #507, .T. ) ;
#10526=CARTESIAN_POINT ( 'NONE',  ( -39.12241743810000116, -66.42264973080000345, 0.4794255386039999456 ) ) ;
#10533=CARTESIAN_POINT ( 'NONE',  ( -41.74999999999475619, -63.24690319806150285, -1.908633995617260437 ) ) ;
#10534=CARTESIAN_POINT ( 'NONE',  ( -38.25000000000000000, -65.00000000000000000, 1.587713240270000048 ) ) ;
#10539=VERTEX_POINT ( 'NONE', #9922 ) ;
#10540=CARTESIAN_POINT ( 'NONE',  ( -37.25000000000000000, -65.00000000000000000, -1.587713240270000048 ) ) ;
#10544=MECHANICAL_DESIGN_GEOMETRIC_PRESENTATION_REPRESENTATION('',(#8689),#4536);
#10554=EDGE_LOOP ( 'NONE', ( #4156, #7455, #6279, #21040 ) ) ;
#10582=ORIENTED_EDGE ( 'NONE', *, *, #17193, .T. ) ;
#10599=ORIENTED_EDGE ( 'NONE', *, *, #11834, .T. ) ;
#10615=ORIENTED_EDGE ( 'NONE', *, *, #5734, .T. ) ;
#10627=ORIENTED_EDGE ( 'NONE', *, *, #22492, .T. ) ;
#10642=CARTESIAN_POINT ( 'NONE',  ( -40.36777568491834245, -65.68647126653578994, -2.245284808034711421 ) ) ;
#10654=CARTESIAN_POINT ( 'NONE',  ( -41.75000000000000000, -65.14977478849999670, 2.684678751729999480 ) ) ;
#10720=CARTESIAN_POINT ( 'NONE',  ( -40.00000000000000000, -94.00000000000000000, 0.000000000000000000 ) ) ;
#10736=CARTESIAN_POINT ( 'NONE',  ( -42.25000000000000000, -63.30468293320000583, 0.7216878364880000563 ) ) ;
#10739=CARTESIAN_POINT ( 'NONE',  ( -38.55000000000000426, -65.14977478849999670, 2.857883832489999776 ) ) ;
#10782=PLANE ( 'NONE',  #15702 ) ;
#10795=PLANE ( 'NONE',  #15401 ) ;
#10807=CARTESIAN_POINT ( 'NONE',  ( -37.75000000000000000, -63.30468293320000583, 0.7216878364859999895 ) ) ;
#10814=CARTESIAN_POINT ( 'NONE',  ( -36.71401968334630794, -65.10234783420575866, -0.07523755576584739702 ) ) ;
#10823=ORIENTED_EDGE ( 'NONE', *, *, #13548, .T. ) ;
#10835=CYLINDRICAL_SURFACE ( 'NONE', #18835, 0.1999999999999987899 ) ;
#10838=VECTOR ( 'NONE', #4347, 1000.000000000000000 ) ;
#10843=ORIENTED_EDGE ( 'NONE', *, *, #9448, .T. ) ;
#10853=EDGE_CURVE ( 'NONE', #28363, #22254, #720, .T. ) ;
#10863=CARTESIAN_POINT ( 'NONE',  ( -41.76016118384315945, -65.69391135771232371, 1.423064894540761349 ) ) ;
#10866=PLANE ( 'NONE',  #13428 ) ;
#10881=CARTESIAN_POINT ( 'NONE',  ( -38.25000000000463984, -63.24690319806150285, 1.908633995616615397 ) ) ;
#10885=CARTESIAN_POINT ( 'NONE',  ( -38.25000000000000000, -65.56519245710001087, 1.769653913539999790 ) ) ;
#10898=VERTEX_POINT ( 'NONE', #3045 ) ;
#10932=CARTESIAN_POINT ( 'NONE',  ( -42.56117883860000006, -65.49083508809999898, 0.5420286502529999551 ) ) ;
#10937=CARTESIAN_POINT ( 'NONE',  ( -42.25000000000000000, -65.63577453799999262, -0.7216878364880000563 ) ) ;
#10942=FACE_OUTER_BOUND ( 'NONE', #12870, .T. ) ;
#10954=CARTESIAN_POINT ( 'NONE',  ( -38.25718401418472325, -65.12549727759254381, -2.739325690388396239 ) ) ;
#10970=CYLINDRICAL_SURFACE ( 'NONE', #8026, 0.1999999999999997891 ) ;
#10975=CARTESIAN_POINT ( 'NONE',  ( -41.75000000000000000, -64.11445222650000630, -2.684678751739999925 ) ) ;
#10996=B_SPLINE_CURVE_WITH_KNOTS ( 'NONE', 3,
 ( #18308, #16102, #24717, #11730, #13777, #20644 ),
 .UNSPECIFIED., .F., .F.,
 ( 4, 2, 4 ),
 ( 0.000000000000000000, 0.5000000000000000000, 1.000000000000000000 ),
 .UNSPECIFIED. ) ;
#10998=ORIENTED_EDGE ( 'NONE', *, *, #938, .F. ) ;
#11002=CARTESIAN_POINT ( 'NONE',  ( -41.78603200349471791, -65.71742637283956867, 1.321057898033102029 ) ) ;
#11034=DIRECTION ( 'NONE',  ( 0.000000000000000000, -1.000000000000000000, 0.000000000000000000 ) ) ;
#11038=CARTESIAN_POINT ( 'NONE',  ( -41.75000000000000000, -63.00000000000000000, 1.587713240270000048 ) ) ;
#11068=CARTESIAN_POINT ( 'NONE',  ( -43.16155280139999917, -65.17124718639999514, 0.1954025812279999996 ) ) ;
#11094=CIRCLE ( 'NONE', #13924, 0.4999999999999985567 ) ;
#11101=CARTESIAN_POINT ( 'NONE',  ( -38.42216747628722828, -65.10234783419650739, -2.883361208460165859 ) ) ;
#11115=VECTOR ( 'NONE', #1158, 1000.000000000000000 ) ;
#11118=FACE_OUTER_BOUND ( 'NONE', #16601, .T. ) ;
#11134=ORIENTED_EDGE ( 'NONE', *, *, #15260, .F. ) ;
#11143=AXIS2_PLACEMENT_3D ( 'NONE', #21233, #10126, #7967 ) ;
#11152=EDGE_CURVE ( 'NONE', #25473, #11263, #14278, .T. ) ;
#11169=VERTEX_POINT ( 'NONE', #25779 ) ;
#11204=CARTESIAN_POINT ( 'NONE',  ( -41.75000000000000000, -63.07912966450000880, 2.684678751729999480 ) ) ;
#11215=CYLINDRICAL_SURFACE ( 'NONE', #17385, 2.999999999999998668 ) ;
#11233=CARTESIAN_POINT ( 'NONE',  ( -39.73574291596239760, -65.71452780515839720, -2.210925124798794883 ) ) ;
#11257=CARTESIAN_POINT ( 'NONE',  ( -36.73717667715042978, -65.11500191527956360, 0.1170746919412273407 ) ) ;
#11260=DIRECTION ( 'NONE',  ( 0.000000000000000000, -1.000000000000000000, 0.000000000000000000 ) ) ;
#11263=VERTEX_POINT ( 'NONE', #6523 ) ;
#11274=AXIS2_PLACEMENT_3D ( 'NONE', #10720, #19083, #21267 ) ;
#11284=DIRECTION ( 'NONE',  ( 0.000000000000000000, 1.000000000000000000, 0.000000000000000000 ) ) ;
#11304=CARTESIAN_POINT ( 'NONE',  ( -38.25000000000000000, -63.00000000000000000, -1.587713240270000048 ) ) ;
#11314=DIRECTION ( 'NONE',  ( 0.000000000000000000, -1.000000000000000000, 0.000000000000000000 ) ) ;
#11319=CARTESIAN_POINT ( 'NONE',  ( -42.06841198963231676, -65.70763704137388572, 0.8557820958490719443 ) ) ;
#11363=CARTESIAN_POINT ( 'NONE',  ( -38.23463116603283396, -65.69529750896734299, -1.411076260621699330 ) ) ;
#11430=DIRECTION ( 'NONE',  ( 0.000000000000000000, -1.000000000000000000, 0.000000000000000000 ) ) ;
#11444=CARTESIAN_POINT ( 'NONE',  ( -37.36725231429999639, -69.50000000000000000, 1.438276615809999992 ) ) ;
#11460=EDGE_CURVE ( 'NONE', #26414, #2354, #22408, .T. ) ;
#11465=CARTESIAN_POINT ( 'NONE',  ( -39.50000000000000000, -65.00000000000000000, -2.309401076760000393 ) ) ;
#11488=ORIENTED_EDGE ( 'NONE', *, *, #2247, .T. ) ;
#11491=CARTESIAN_POINT ( 'NONE',  ( -41.75000000000000000, -65.19264941160000149, -2.595760183529999932 ) ) ;
#11509=CARTESIAN_POINT ( 'NONE',  ( -38.09325189486211372, -65.74401273906202903, -1.048281052909203925 ) ) ;
#11511=ORIENTED_EDGE ( 'NONE', *, *, #2247, .F. ) ;
#11528=EDGE_CURVE ( 'NONE', #28438, #26536, #23741, .T. ) ;
#11544=CARTESIAN_POINT ( 'NONE',  ( -36.74526444670264169, -63.06504043304235552, 0.1318650859689453059 ) ) ;
#11553=CARTESIAN_POINT ( 'NONE',  ( -38.25943422533623561, -65.12255024415871674, -2.746802154549074615 ) ) ;
#11575=AXIS2_PLACEMENT_3D ( 'NONE', #23880, #24018, #3917 ) ;
#11603=DIRECTION ( 'NONE',  ( 1.000000000000000000, 0.000000000000000000, 0.000000000000000000 ) ) ;
#11642=CARTESIAN_POINT ( 'NONE',  ( -38.44999999999999574, -65.00000000000000000, -2.684678751729999480 ) ) ;
#11655=CARTESIAN_POINT ( 'NONE',  ( -37.82487616201437675, -65.66931566142197596, -0.7649176087804624435 ) ) ;
#11673=SHAPE_REPRESENTATION_RELATIONSHIP ( 'NONE' , 'NONE' ,  #24690, #23754 ) ;
#11675=ADVANCED_FACE ( 'NONE', ( #27397 ), #14654, .T. ) ;
#11692=CARTESIAN_POINT ( 'NONE',  ( -43.25079786316290154, -65.12158389262772573, 0.1356225091523582948 ) ) ;
#11693=CARTESIAN_POINT ( 'NONE',  ( -36.76943391352939727, -63.07120704560310998, -0.1555577424969001310 ) ) ;
#11701=DIRECTION ( 'NONE',  ( 0.000000000000000000, 1.000000000000000000, 0.000000000000000000 ) ) ;
#11703=CARTESIAN_POINT ( 'NONE',  ( -40.00000000000000000, -69.50000000000000000, 0.000000000000000000 ) ) ;
#11730=CARTESIAN_POINT ( 'NONE',  ( -38.23579088423348082, -63.33604893235135336, 1.392788587647418197 ) ) ;
#11740=FACE_OUTER_BOUND ( 'NONE', #8057, .T. ) ;
#11776=FACE_OUTER_BOUND ( 'NONE', #16898, .T. ) ;
#11813=ORIENTED_EDGE ( 'NONE', *, *, #23023, .F. ) ;
#11834=EDGE_CURVE ( 'NONE', #18068, #11263, #20236, .T. ) ;
#11842=ORIENTED_EDGE ( 'NONE', *, *, #23468, .F. ) ;
#11875=ORIENTED_EDGE ( 'NONE', *, *, #11834, .F. ) ;
#11877=EDGE_CURVE ( 'NONE', #10898, #26111, #1815, .T. ) ;
#11889=DIRECTION ( 'NONE',  ( 0.000000000000000000, -1.000000000000000000, 0.000000000000000000 ) ) ;
#11900=B_SPLINE_CURVE_WITH_KNOTS ( 'NONE', 3,
 ( #17608, #21687, #24453, #14965 ),
 .UNSPECIFIED., .F., .F.,
 ( 4, 4 ),
 ( 0.000000000000000000, 1.000000000000000000 ),
 .UNSPECIFIED. ) ;
#11926=ORIENTED_EDGE ( 'NONE', *, *, #17856, .F. ) ;
#11957=CARTESIAN_POINT ( 'NONE',  ( -41.75000000000000000, -64.47022873560000278, 1.587713240270000048 ) ) ;
#11988=DIRECTION ( 'NONE',  ( 0.000000000000000000, -1.000000000000000000, 0.000000000000000000 ) ) ;
#12066=TOROIDAL_SURFACE ( 'NONE', #20932, 4.500000000000000000, 0.5000000000000000000 ) ;
#12077=EDGE_CURVE ( 'NONE', #813, #25610, #17478, .T. ) ;
#12078=EDGE_LOOP ( 'NONE', ( #13679, #11511, #15717, #1810 ) ) ;
#12084=CARTESIAN_POINT ( 'NONE',  ( -36.79999999999999716, -63.07912966450000880, -0.1732050807570000017 ) ) ;
#12092=ORIENTED_EDGE ( 'NONE', *, *, #22182, .T. ) ;
#12102=CARTESIAN_POINT ( 'NONE',  ( -40.00000000000000000, -63.50000000000000000, 0.000000000000000000 ) ) ;
#12189=CARTESIAN_POINT ( 'NONE',  ( -38.55000000000000426, -64.11445222650000630, -2.857883832489999776 ) ) ;
#12212=CARTESIAN_POINT ( 'NONE',  ( -36.79999999999999716, -63.07912966450000880, 0.1732050807570000017 ) ) ;
#12223=AXIS2_PLACEMENT_3D ( 'NONE', #13995, #5400, #9897 ) ;
#12241=B_SPLINE_CURVE_WITH_KNOTS ( 'NONE', 3,
 ( #7459, #16607, #27563, #12084 ),
 .UNSPECIFIED., .F., .F.,
 ( 4, 4 ),
 ( 0.000000000000000000, 1.000000000000000000 ),
 .UNSPECIFIED. ) ;
#12243=EDGE_CURVE ( 'NONE', #2354, #9232, #11094, .T. ) ;
#12268=CARTESIAN_POINT ( 'NONE',  ( -43.30001519683280264, -65.09473604209610187, -0.03967052575387554347 ) ) ;
#12283=VERTEX_POINT ( 'NONE', #25922 ) ;
#12318=EDGE_CURVE ( 'NONE', #14297, #5567, #11900, .T. ) ;
#12326=PLANE ( 'NONE',  #2814 ) ;
#12332=CARTESIAN_POINT ( 'NONE',  ( -40.00000000000000000, -69.00000000000000000, 0.000000000000000000 ) ) ;
#12385=DIRECTION ( 'NONE',  ( 0.000000000000000000, -1.000000000000000000, 0.000000000000000000 ) ) ;
#12422=CARTESIAN_POINT ( 'NONE',  ( -37.75000000000000000, -63.30468293320000583, 0.7216878364859999895 ) ) ;
#12475=CARTESIAN_POINT ( 'NONE',  ( -41.88392290732132750, -65.74504297427023403, -1.085364455063224209 ) ) ;
#12494=CARTESIAN_POINT ( 'NONE',  ( -43.20000000000000284, -63.07912966450000880, 0.1732050807559999961 ) ) ;
#12542=VECTOR ( 'NONE', #22533, 1000.000000000000000 ) ;
#12544=B_SPLINE_CURVE_WITH_KNOTS ( 'NONE', 3,
 ( #6087, #23876, #10306, #12494 ),
 .UNSPECIFIED., .F., .F.,
 ( 4, 4 ),
 ( 0.000000000000000000, 1.000000000000000000 ),
 .UNSPECIFIED. ) ;
#12550=CARTESIAN_POINT ( 'NONE',  ( -37.10038231309999901, -65.31510159580000163, 0.3466308900749999755 ) ) ;
#12599=DIRECTION ( 'NONE',  ( 0.000000000000000000, -1.000000000000000000, 0.000000000000000000 ) ) ;
#12615=EDGE_LOOP ( 'NONE', ( #3516, #10823 ) ) ;
#12618=CARTESIAN_POINT ( 'NONE',  ( -41.53002200404621647, -65.11500191528324422, -2.884225231620696661 ) ) ;
#12627=ORIENTED_EDGE ( 'NONE', *, *, #9124, .T. ) ;
#12645=CARTESIAN_POINT ( 'NONE',  ( -38.29487672305123169, -65.09473114940418270, 2.826095656349198570 ) ) ;
#12646=CARTESIAN_POINT ( 'NONE',  ( -44.38791280949999418, -69.00000000000000000, -2.397127693020000283 ) ) ;
#12653=VECTOR ( 'NONE', #1246, 1000.000000000000000 ) ;
#12669=ORIENTED_EDGE ( 'NONE', *, *, #22616, .F. ) ;
#12695=CIRCLE ( 'NONE', #6196, 3.000000000000002665 ) ;
#12698=CARTESIAN_POINT ( 'NONE',  ( -39.80580048936597137, -65.72850285331089992, -2.193980430793042391 ) ) ;
#12728=CARTESIAN_POINT ( 'NONE',  ( -38.55000000000000426, -63.07912966450000880, 2.857883832489999776 ) ) ;
#12740=ORIENTED_EDGE ( 'NONE', *, *, #15889, .T. ) ;
#12755=EDGE_LOOP ( 'NONE', ( #14455, #6202, #26036, #16275 ) ) ;
#12759=ORIENTED_EDGE ( 'NONE', *, *, #1960, .F. ) ;
#12771=CARTESIAN_POINT ( 'NONE',  ( -38.25764126207506877, -63.06523941402393518, 2.751386478887667408 ) ) ;
#12788=CARTESIAN_POINT ( 'NONE',  ( -38.25000000000000000, -65.14977478849999670, -2.684678751729999480 ) ) ;
#12789=ORIENTED_EDGE ( 'NONE', *, *, #20503, .F. ) ;
#12813=ORIENTED_EDGE ( 'NONE', *, *, #19207, .T. ) ;
#12821=CARTESIAN_POINT ( 'NONE',  ( -41.74235873792772367, -63.06523941402236488, -2.751386478892827281 ) ) ;
#12830=CARTESIAN_POINT ( 'NONE',  ( -36.83844719860000083, -65.17124718639999514, 0.1954025812279999996 ) ) ;
#12852=ORIENTED_EDGE ( 'NONE', *, *, #7160, .F. ) ;
#12859=LINE ( 'NONE', #10526, #28105 ) ;
#12870=EDGE_LOOP ( 'NONE', ( #19709, #951, #16894, #354 ) ) ;
#12873=DIRECTION ( 'NONE',  ( 0.000000000000000000, -1.000000000000000000, 0.000000000000000000 ) ) ;
#12916=CARTESIAN_POINT ( 'NONE',  ( -39.50000000000000000, -63.30468293320000583, 2.309401076760000393 ) ) ;
#12926=AXIS2_PLACEMENT_3D ( 'NONE', #9731, #18643, #7982 ) ;
#12931=CARTESIAN_POINT ( 'NONE',  ( -38.25000000000000000, -65.63577453799999262, 1.587713240270000048 ) ) ;
#12961=ORIENTED_EDGE ( 'NONE', *, *, #19207, .F. ) ;
#12977=ORIENTED_EDGE ( 'NONE', *, *, #24434, .T. ) ;
#12986=CARTESIAN_POINT ( 'NONE',  ( -41.91080735079999897, -65.74290444429999525, -1.043878813350000101 ) ) ;
#12987=ORIENTED_EDGE ( 'NONE', *, *, #23023, .T. ) ;
#13029=FACE_OUTER_BOUND ( 'NONE', #13792, .T. ) ;
#13066=EDGE_CURVE ( 'NONE', #623, #9249, #28199, .T. ) ;
#13074=CARTESIAN_POINT ( 'NONE',  ( -41.74999999998716760, -63.32273534313992513, -1.487446372639924963 ) ) ;
#13109=ORIENTED_EDGE ( 'NONE', *, *, #22877, .T. ) ;
#13111=CARTESIAN_POINT ( 'NONE',  ( -38.25000000000000000, -63.30468293320000583, 1.587713240270000048 ) ) ;
#13116=CARTESIAN_POINT ( 'NONE',  ( -38.25000000000000000, -63.24880261863425090, -1.898084215915099460 ) ) ;
#13159=PRODUCT ( 'Housing Torx Attachment Screw', 'Housing Torx Attachment Screw', '', ( #22888 ) ) ;
#13184=FACE_OUTER_BOUND ( 'NONE', #28068, .T. ) ;
#13248=CARTESIAN_POINT ( 'NONE',  ( -42.56117883860000006, -65.49083508809999898, -0.5420286502529999551 ) ) ;
#13281=CARTESIAN_POINT ( 'NONE',  ( -42.25000000000000000, -65.63577453799999262, 0.7216878364880000563 ) ) ;
#13282=CARTESIAN_POINT ( 'NONE',  ( -41.99796191249483712, -65.72812594248435403, -0.9281908455079398435 ) ) ;
#13285=PLANE ( 'NONE',  #8943 ) ;
#13323=ORIENTED_EDGE ( 'NONE', *, *, #13548, .F. ) ;
#13334=CARTESIAN_POINT ( 'NONE',  ( -43.94912152850000098, -63.50000000000000000, -2.157414923720000210 ) ) ;
#13419=FACE_OUTER_BOUND ( 'NONE', #2375, .T. ) ;
#13427=CARTESIAN_POINT ( 'NONE',  ( -43.08431406180000067, -65.21397798589998729, 0.2399963883289999989 ) ) ;
#13428=AXIS2_PLACEMENT_3D ( 'NONE', #1464, #6534, #15391 ) ;
#13432=DIRECTION ( 'NONE',  ( -0.5000000000001900702, 0.000000000000000000, 0.8660254037843290176 ) ) ;
#13493=CIRCLE ( 'NONE', #20001, 3.000000000000002665 ) ;
#13547=FACE_OUTER_BOUND ( 'NONE', #5805, .T. ) ;
#13548=EDGE_CURVE ( 'NONE', #17502, #20283, #27841, .T. ) ;
#13551=CARTESIAN_POINT ( 'NONE',  ( -41.75000000000000000, -63.30468293320000583, 1.587713240270000048 ) ) ;
#13559=CARTESIAN_POINT ( 'NONE',  ( -38.25000000000000000, -65.63577453799999262, -1.587713240270000048 ) ) ;
#13569=DIRECTION ( 'NONE',  ( 0.8775825618903724257, 0.000000000000000000, 0.4794255386042036160 ) ) ;
#13610=EDGE_CURVE ( 'NONE', #24058, #10217, #888, .T. ) ;
#13616=EDGE_CURVE ( 'NONE', #25860, #11169, #9228, .T. ) ;
#13636=CARTESIAN_POINT ( 'NONE',  ( -41.59490899353561133, -65.09473114940422533, 2.889727902555501160 ) ) ;
#13663=EDGE_LOOP ( 'NONE', ( #9306, #6075, #9592, #22971, #5901, #21069, #10140, #13990, #18267, #12977, #23292, #21280, #4667, #5183, #13323, #366 ) ) ;
#13671=CARTESIAN_POINT ( 'NONE',  ( -41.91080743279999865, -63.35440207070000440, -1.043878858150000033 ) ) ;
#13679=ORIENTED_EDGE ( 'NONE', *, *, #5241, .T. ) ;
#13712=CARTESIAN_POINT ( 'NONE',  ( -38.16136311219324284, -65.74402559148357739, -1.166215138813985419 ) ) ;
#13753=CARTESIAN_POINT ( 'NONE',  ( -38.25000000000000000, -63.07912966450000880, -2.684678751729999480 ) ) ;
#13755=DIRECTION ( 'NONE',  ( 0.8775825618903723147, 0.000000000000000000, 0.4794255386042037825 ) ) ;
#13777=CARTESIAN_POINT ( 'NONE',  ( -38.25000000001283951, -63.32273534313050334, 1.487446372692276864 ) ) ;
#13792=EDGE_LOOP ( 'NONE', ( #12961, #6528, #2494, #2122 ) ) ;
#13806=ORIENTED_EDGE ( 'NONE', *, *, #16851, .F. ) ;
#13818=DIRECTION ( 'NONE',  ( 0.000000000000000000, -1.000000000000000000, 0.000000000000000000 ) ) ;
#13840=CARTESIAN_POINT ( 'NONE',  ( -41.75000000000000000, -65.41419836839999391, -2.121055962339999823 ) ) ;
#13851=CARTESIAN_POINT ( 'NONE',  ( -41.37299426109999700, -65.19264941160000149, -2.813424548380000001 ) ) ;
#13856=CARTESIAN_POINT ( 'NONE',  ( -37.89028998459014019, -65.69483747913999139, -0.8156460645458384340 ) ) ;
#13859=CARTESIAN_POINT ( 'NONE',  ( -38.07292563641772887, -63.35495820213566986, -1.012765098742579362 ) ) ;
#13913=B_SPLINE_CURVE_WITH_KNOTS ( 'NONE', 3,
 ( #6696, #15557, #12645, #19370, #18200, #4647 ),
 .UNSPECIFIED., .F., .F.,
 ( 4, 2, 4 ),
 ( 0.000000000000000000, 0.5000000000000000000, 1.000000000000000000 ),
 .UNSPECIFIED. ) ;
#13924=AXIS2_PLACEMENT_3D ( 'NONE', #25649, #21270, #3776 ) ;
#13928=CARTESIAN_POINT ( 'NONE',  ( -41.45000000000000284, -63.07912966450000880, -2.857883832489999776 ) ) ;
#13929=DIRECTION ( 'NONE',  ( 1.000000000000000000, 0.000000000000000000, 0.000000000000000000 ) ) ;
#13967=VERTEX_POINT ( 'NONE', #24428 ) ;
#13974=CARTESIAN_POINT ( 'NONE',  ( -39.18882116139999994, -65.49083508809999898, -2.489060262989999828 ) ) ;
#13985=AXIS2_PLACEMENT_3D ( 'NONE', #26671, #11034, #6858 ) ;
#13990=ORIENTED_EDGE ( 'NONE', *, *, #24213, .F. ) ;
#13995=CARTESIAN_POINT ( 'NONE',  ( -36.92846103339999786, -69.50000000000000000, 1.677989385109999843 ) ) ;
#14010=B_SPLINE_CURVE_WITH_KNOTS ( 'NONE', 3,
 ( #24450, #6679, #26492, #6371, #24010, #6233, #11319, #15388, #21974, #4345, #28655, #1877, #8557, #2024, #6530, #11002, #4044, #10863, #19633, #8686 ),
 .UNSPECIFIED., .F., .F.,
 ( 4, 2, 1, 2, 2, 2, 2, 1, 2, 2, 4 ),
 ( 0.000000000000000000, 0.1250000000000299760, 0.1875000000000449640, 0.2187500000000577038, 0.2500000000000704437, 0.5000000000000650591, 0.6250000000000579536, 0.6875000000000579536, 0.7187500000000521805, 0.7500000000000465183, 1.000000000000000000 ),
 .UNSPECIFIED. ) ;
#14076=DIRECTION ( 'NONE',  ( -0.5000000000001882938, 0.000000000000000000, -0.8660254037843300168 ) ) ;
#14123=VERTEX_POINT ( 'NONE', #17112 ) ;
#14127=CARTESIAN_POINT ( 'NONE',  ( -38.85038231309999901, -65.31510159580000163, -2.684458023169999930 ) ) ;
#14144=LINE ( 'NONE', #9321, #5719 ) ;
#14189=CARTESIAN_POINT ( 'NONE',  ( -43.20000000000000284, -65.14977478849999670, -0.1732050807570000017 ) ) ;
#14208=EDGE_CURVE ( 'NONE', #17600, #11169, #20434, .T. ) ;
#14210=CARTESIAN_POINT ( 'NONE',  ( -37.36725231429999639, -94.00000000000000000, 1.438276615809999992 ) ) ;
#14266=VERTEX_POINT ( 'NONE', #1825 ) ;
#14269=CARTESIAN_POINT ( 'NONE',  ( -41.74999999999999289, -65.67306013599217351, -1.491601497600667958 ) ) ;
#14278=LINE ( 'NONE', #20849, #4236 ) ;
#14283=ORIENTED_EDGE ( 'NONE', *, *, #5146, .T. ) ;
#14285=DIRECTION ( 'NONE',  ( 1.000000000000000000, 0.000000000000000000, 0.000000000000000000 ) ) ;
#14297=VERTEX_POINT ( 'NONE', #24395 ) ;
#14312=CONICAL_SURFACE ( 'NONE', #6386, 1.732050807582486307, 1.047197551199999799 ) ;
#14336=DIRECTION ( 'NONE',  ( 0.8775825618903724257, 0.000000000000000000, 0.4794255386042036160 ) ) ;
#14357=CARTESIAN_POINT ( 'NONE',  ( -42.25000000000000000, -63.00000000000000000, -0.7216878364880000563 ) ) ;
#14376=ORIENTED_EDGE ( 'NONE', *, *, #23338, .T. ) ;
#14444=APPLICATION_CONTEXT ( 'automotive_design' ) ;
#14455=ORIENTED_EDGE ( 'NONE', *, *, #24505, .T. ) ;
#14470=CARTESIAN_POINT ( 'NONE',  ( -41.61797703107799151, -63.05366661936065498, -2.876041293750446481 ) ) ;
#14482=AXIS2_PLACEMENT_3D ( 'NONE', #22311, #26838, #6869 ) ;
#14506=CARTESIAN_POINT ( 'NONE',  ( -41.58361464086270587, -63.05597747387622576, 2.885209034396454708 ) ) ;
#14512=EDGE_CURVE ( 'NONE', #13967, #23133, #18233, .T. ) ;
#14547=ORIENTED_EDGE ( 'NONE', *, *, #2594, .F. ) ;
#14549=VERTEX_POINT ( 'NONE', #13111 ) ;
#14570=CYLINDRICAL_SURFACE ( 'NONE', #27072, 0.1999999999999996780 ) ;
#14588=ORIENTED_EDGE ( 'NONE', *, *, #4208, .T. ) ;
#14593=LINE ( 'NONE', #2980, #646 ) ;
#14594=VECTOR ( 'NONE', #15992, 1000.000000000000000 ) ;
#14634=B_SPLINE_CURVE_WITH_KNOTS ( 'NONE', 3,
 ( #8739, #13116, #19540, #6134 ),
 .UNSPECIFIED., .F., .F.,
 ( 4, 4 ),
 ( 0.000000000000000000, 1.000000000000000000 ),
 .UNSPECIFIED. ) ;
#14654=CYLINDRICAL_SURFACE ( 'NONE', #16838, 1.000000000000000888 ) ;
#14686=ORIENTED_EDGE ( 'NONE', *, *, #5734, .F. ) ;
#14688=ORIENTED_EDGE ( 'NONE', *, *, #24752, .F. ) ;
#14692=ADVANCED_FACE ( 'NONE', ( #23595 ), #24147, .F. ) ;
#14702=VERTEX_POINT ( 'NONE', #6382 ) ;
#14756=EDGE_CURVE ( 'NONE', #14297, #623, #15586, .T. ) ;
#14778=CARTESIAN_POINT ( 'NONE',  ( -40.16286846138842748, -63.35496709432901241, -2.175426692284139651 ) ) ;
#14781=EDGE_LOOP ( 'NONE', ( #21222, #3757 ) ) ;
#14832=VECTOR ( 'NONE', #24796, 1000.000000000000000 ) ;
#14887=CARTESIAN_POINT ( 'NONE',  ( -40.09065349277244650, -65.74402559150934167, -2.175413822581698575 ) ) ;
#14894=AXIS2_PLACEMENT_3D ( 'NONE', #26573, #15176, #24089 ) ;
#14945=VECTOR ( 'NONE', #17132, 1000.000000000000000 ) ;
#14956=VERTEX_POINT ( 'NONE', #9871 ) ;
#14965=CARTESIAN_POINT ( 'NONE',  ( -42.25000000000000000, -63.30468293320000583, -0.7216878364880000563 ) ) ;
#14981=CARTESIAN_POINT ( 'NONE',  ( -38.25000000000000000, -65.17124718639999514, 2.640283750789999662 ) ) ;
#15039=ADVANCED_FACE ( 'NONE', ( #10278 ), #3332, .F. ) ;
#15069=DIRECTION ( 'NONE',  ( -0.5000000000001884048, 0.000000000000000000, 0.8660254037843300168 ) ) ;
#15105=ORIENTED_EDGE ( 'NONE', *, *, #27519, .T. ) ;
#15116=CARTESIAN_POINT ( 'NONE',  ( -38.25000000000000000, -65.49083508809999898, 1.947031612740000028 ) ) ;
#15123=ORIENTED_EDGE ( 'NONE', *, *, #24434, .F. ) ;
#15129=CARTESIAN_POINT ( 'NONE',  ( -42.71188834620000563, -65.41419836839999391, -0.4550164754569999692 ) ) ;
#15139=CARTESIAN_POINT ( 'NONE',  ( -40.50000000000000000, -65.63577453799999262, 2.309401076760000393 ) ) ;
#15162=CARTESIAN_POINT ( 'NONE',  ( -39.74899213917685614, -65.71745250375693104, -2.207370884887611684 ) ) ;
#15176=DIRECTION ( 'NONE',  ( 0.000000000000000000, 1.000000000000000000, 0.000000000000000000 ) ) ;
#15182=CARTESIAN_POINT ( 'NONE',  ( -36.69998480316156275, -65.09473604209287600, 0.03967052571942218664 ) ) ;
#15190=VECTOR ( 'NONE', #18192, 1000.000000000000000 ) ;
#15192=CIRCLE ( 'NONE', #4046, 4.499999999999997335 ) ;
#15195=ADVANCED_FACE ( 'NONE', ( #5448 ), #16654, .T. ) ;
#15200=DIRECTION ( 'NONE',  ( 1.000000000000000000, 0.000000000000000000, 0.000000000000000000 ) ) ;
#15208=CARTESIAN_POINT ( 'NONE',  ( -38.25000000000000000, -65.63577453799999262, 1.587713240270000048 ) ) ;
#15209=ORIENTED_EDGE ( 'NONE', *, *, #1721, .T. ) ;
#15257=CARTESIAN_POINT ( 'NONE',  ( -38.25000000000000000, -65.14977478849999670, 2.684678751729999480 ) ) ;
#15260=EDGE_CURVE ( 'NONE', #21937, #8977, #21385, .T. ) ;
#15262=B_SPLINE_CURVE_WITH_KNOTS ( 'NONE', 3,
 ( #7954, #10112, #21221, #14506, #5622, #9985, #5203, #1273, #27653, #23544 ),
 .UNSPECIFIED., .F., .F.,
 ( 4, 2, 2, 2, 4 ),
 ( 0.000000000000000000, 0.2500000000000000000, 0.5000000000000000000, 0.7500000000000000000, 1.000000000000000000 ),
 .UNSPECIFIED. ) ;
#15300=EDGE_CURVE ( 'NONE', #14266, #14123, #2606, .T. ) ;
#15339=APPLICATION_CONTEXT ( 'automotive_design' ) ;
#15340=CARTESIAN_POINT ( 'NONE',  ( -39.23121085047505829, -63.24880261863123820, 2.464586564592250895 ) ) ;
#15354=DIRECTION ( 'NONE',  ( -1.000000000000000000, 0.000000000000000000, -2.168404344971021884E-15 ) ) ;
#15375=VERTEX_POINT ( 'NONE', #18910 ) ;
#15388=CARTESIAN_POINT ( 'NONE',  ( -42.06204301354549102, -65.70971443686121916, 0.8617459228010823091 ) ) ;
#15389=CARTESIAN_POINT ( 'NONE',  ( -42.83545581620172271, -63.17361819572899151, -0.3836747634055225897 ) ) ;
#15391=DIRECTION ( 'NONE',  ( 0.000000000000000000, 1.000000000000000000, 0.000000000000000000 ) ) ;
#15393=EDGE_CURVE ( 'NONE', #20440, #7086, #16711, .T. ) ;
#15401=AXIS2_PLACEMENT_3D ( 'NONE', #19292, #8209, #6447 ) ;
#15409=ADVANCED_FACE ( 'NONE', ( #9714 ), #12326, .T. ) ;
#15430=ADVANCED_FACE ( 'NONE', ( #7566 ), #9860, .F. ) ;
#15435=ORIENTED_EDGE ( 'NONE', *, *, #26924, .T. ) ;
#15471=CARTESIAN_POINT ( 'NONE',  ( -40.00000000000000000, -69.50000000000000000, 0.000000000000000000 ) ) ;
#15482=CARTESIAN_POINT ( 'NONE',  ( -36.74089255422700262, -65.11704020643968249, 0.1219423816524388415 ) ) ;
#15487=CARTESIAN_POINT ( 'NONE',  ( -38.36731331058076933, -65.09474816371883321, -2.867870865955927329 ) ) ;
#15529=EDGE_CURVE ( 'NONE', #26111, #813, #4746, .T. ) ;
#15548=LINE ( 'NONE', #17756, #14594 ) ;
#15552=CARTESIAN_POINT ( 'NONE',  ( -41.76420911575942796, -63.33604893236084621, -1.392788587596942351 ) ) ;
#15557=CARTESIAN_POINT ( 'NONE',  ( -38.25000000000000000, -65.11307468787711628, 2.760557608143826780 ) ) ;
#15586=B_SPLINE_CURVE_WITH_KNOTS ( 'NONE', 3,
 ( #13671, #15697, #2318, #15552, #13074, #22132 ),
 .UNSPECIFIED., .F., .F.,
 ( 4, 2, 4 ),
 ( 0.000000000000000000, 0.5000000000000000000, 1.000000000000000000 ),
 .UNSPECIFIED. ) ;
#15592=ORIENTED_EDGE ( 'NONE', *, *, #23468, .T. ) ;
#15614=AXIS2_PLACEMENT_3D ( 'NONE', #27651, #11889, #855 ) ;
#15636=CARTESIAN_POINT ( 'NONE',  ( -38.52200237161242313, -65.13413837704243292, -2.874048270801004890 ) ) ;
#15650=DIRECTION ( 'NONE',  ( 0.000000000000000000, -1.000000000000000000, 0.000000000000000000 ) ) ;
#15689=CARTESIAN_POINT ( 'NONE',  ( -38.55000000000000426, -63.07912966450000880, -2.857883832489999776 ) ) ;
#15697=CARTESIAN_POINT ( 'NONE',  ( -41.85858414364702185, -63.35633004489629627, -1.124464781979226613 ) ) ;
#15702=AXIS2_PLACEMENT_3D ( 'NONE', #19694, #8898, #8617 ) ;
#15717=ORIENTED_EDGE ( 'NONE', *, *, #10853, .F. ) ;
#15758=CARTESIAN_POINT ( 'NONE',  ( -39.50000000000000000, -65.63577453799999262, -2.309401076760000393 ) ) ;
#15799=CARTESIAN_POINT ( 'NONE',  ( -40.00000000000000000, -69.50000000000000000, 0.000000000000000000 ) ) ;
#15824=VECTOR ( 'NONE', #5570, 1000.000000000000114 ) ;
#15847=ORIENTED_EDGE ( 'NONE', *, *, #12318, .T. ) ;
#15868=SHAPE_DEFINITION_REPRESENTATION ( #24339, #24690 ) ;
#15889=EDGE_CURVE ( 'NONE', #11169, #25860, #15192, .T. ) ;
#15890=CARTESIAN_POINT ( 'NONE',  ( -38.22863009216007413, -65.70299785168744222, -1.381847430537364030 ) ) ;
#15976=CIRCLE ( 'NONE', #17840, 2.000000000000001776 ) ;
#15992=DIRECTION ( 'NONE',  ( 0.000000000000000000, -1.000000000000000000, 0.000000000000000000 ) ) ;
#15995=ORIENTED_EDGE ( 'NONE', *, *, #15393, .F. ) ;
#16000=B_SPLINE_CURVE_WITH_KNOTS ( 'NONE', 5,
 ( #17482, #17922, #23894, #6394, #26661, #3930, #163, #4212, #10739 ),
 .UNSPECIFIED., .F., .F.,
 ( 6, 3, 6 ),
 ( 0.000000000000000000, 1.237573681330000008, 1.566718891460000096 ),
 .UNSPECIFIED. ) ;
#16036=CARTESIAN_POINT ( 'NONE',  ( -37.97905434469389263, -65.72207046438377631, -0.9031576581934117609 ) ) ;
#16071=MANIFOLD_SOLID_BREP ( 'Screw Set - M6-18mm TorxKey', #5386 ) ;
#16075=CARTESIAN_POINT ( 'NONE',  ( -37.98130312831552402, -65.72281103701608629, 0.9050787996994155149 ) ) ;
#16093=CARTESIAN_POINT ( 'NONE',  ( -37.89522944376288649, -63.33487562142549621, 0.8055360949360760303 ) ) ;
#16102=CARTESIAN_POINT ( 'NONE',  ( -38.14141585637982956, -63.35633004489675812, 1.124464782024710674 ) ) ;
#16117=B_SPLINE_CURVE_WITH_KNOTS ( 'NONE', 3,
 ( #10148, #12475, #21389, #10017, #27811, #5521, #16595, #23446, #19069, #23712, #14269, #28088 ),
 .UNSPECIFIED., .F., .F.,
 ( 4, 2, 1, 1, 2, 2, 4 ),
 ( 0.000000000000000000, 0.2499999999999843459, 0.3749999999999700240, 0.4374999999999628630, 0.4687499999999649170, 0.4999999999999670264, 1.000000000000000000 ),
 .UNSPECIFIED. ) ;
#16152=CARTESIAN_POINT ( 'NONE',  ( -39.50000000000000000, -65.63577453799999262, -2.309401076760000393 ) ) ;
#16176=EDGE_LOOP ( 'NONE', ( #9587, #1085, #38, #25034 ) ) ;
#16182=CARTESIAN_POINT ( 'NONE',  ( -38.02338021417244107, -63.35089350796872765, -0.9476039871582396801 ) ) ;
#16201=DIRECTION ( 'NONE',  ( 0.8775825618903724257, 0.000000000000000000, 0.4794255386042037825 ) ) ;
#16211=CARTESIAN_POINT ( 'NONE',  ( -36.79999999999999716, -63.07912966450000880, 0.1732050807570000017 ) ) ;
#16235=DIRECTION ( 'NONE',  ( 0.000000000000000000, -1.000000000000000000, 0.000000000000000000 ) ) ;
#16244=ORIENTED_EDGE ( 'NONE', *, *, #18279, .F. ) ;
#16275=ORIENTED_EDGE ( 'NONE', *, *, #2048, .F. ) ;
#16293=ORIENTED_EDGE ( 'NONE', *, *, #11877, .F. ) ;
#16344=CARTESIAN_POINT ( 'NONE',  ( -38.14025503984489518, -65.74398723832256053, 1.129426529332413720 ) ) ;
#16358=ADVANCED_FACE ( 'NONE', ( #21792 ), #10835, .F. ) ;
#16373=CARTESIAN_POINT ( 'NONE',  ( -37.87497158468980274, -65.68892059713630260, 0.8034379168488015033 ) ) ;
#16379=ORIENTED_EDGE ( 'NONE', *, *, #2594, .T. ) ;
#16389=EDGE_CURVE ( 'NONE', #6476, #26414, #2869, .T. ) ;
#16470=DIRECTION ( 'NONE',  ( 0.000000000000000000, -1.000000000000000000, 0.000000000000000000 ) ) ;
#16491=CARTESIAN_POINT ( 'NONE',  ( -38.23614497916284449, -65.70026997502627353, 1.401764440867459660 ) ) ;
#16523=CARTESIAN_POINT ( 'NONE',  ( -37.95930193997842395, -65.71630926063573952, 0.8827409024611270194 ) ) ;
#16524=CARTESIAN_POINT ( 'NONE',  ( -40.00000000000000000, -66.00000000000000000, 0.000000000000000000 ) ) ;
#16562=CARTESIAN_POINT ( 'NONE',  ( -41.41155280139999917, -65.17124718639999514, 2.835686332019999867 ) ) ;
#16587=B_SPLINE_CURVE_WITH_KNOTS ( 'NONE', 3,
 ( #2554, #25134, #2994, #7355, #4872, #376, #9664, #9220, #27315, #13753 ),
 .UNSPECIFIED., .F., .F.,
 ( 4, 2, 2, 2, 4 ),
 ( 0.000000000000000000, 0.2500000000000000000, 0.5000000000000000000, 0.7500000000000000000, 1.000000000000000000 ),
 .UNSPECIFIED. ) ;
#16595=CARTESIAN_POINT ( 'NONE',  ( -41.79353403746807061, -65.72247384671341308, -1.295796974283231151 ) ) ;
#16601=EDGE_LOOP ( 'NONE', ( #1210, #20187 ) ) ;
#16607=CARTESIAN_POINT ( 'NONE',  ( -37.47207447326633201, -63.24690319806014571, -0.5612274588096003436 ) ) ;
#16637=LINE ( 'NONE', #25817, #15824 ) ;
#16654=CYLINDRICAL_SURFACE ( 'NONE', #27000, 0.9999999999999990008 ) ;
#16669=CARTESIAN_POINT ( 'NONE',  ( -40.50000000000000000, -65.63577453799999262, -2.309401076760000393 ) ) ;
#16689=CARTESIAN_POINT ( 'NONE',  ( -38.25000000000000000, -65.63577453799999262, -1.587713240270000048 ) ) ;
#16711=LINE ( 'NONE', #18478, #11115 ) ;
#16721=ORIENTED_EDGE ( 'NONE', *, *, #2664, .F. ) ;
#16739=UNCERTAINTY_MEASURE_WITH_UNIT (LENGTH_MEASURE( 1.000000000000000082E-05 ), #7496, 'distance_accuracy_value', 'NONE');
#16753=CARTESIAN_POINT ( 'NONE',  ( -41.75516512379999767, -65.84529946160000691, -0.9588510772079998912 ) ) ;
#16764=DIRECTION ( 'NONE',  ( 0.000000000000000000, -1.000000000000000000, 0.000000000000000000 ) ) ;
#16774=EDGE_CURVE ( 'NONE', #10217, #25894, #9236, .T. ) ;
#16781=ORIENTED_EDGE ( 'NONE', *, *, #11152, .T. ) ;
#16824=B_SPLINE_CURVE_WITH_KNOTS ( 'NONE', 5,
 ( #13281, #20285, #10932, #9056, #9198, #13427, #22632, #11068, #506 ),
 .UNSPECIFIED., .F., .F.,
 ( 6, 3, 6 ),
 ( 0.000000000000000000, 1.237573681340000009, 1.566718891480000098 ),
 .UNSPECIFIED. ) ;
#16838=AXIS2_PLACEMENT_3D ( 'NONE', #23548, #9308, #3080 ) ;
#16847=EDGE_CURVE ( 'NONE', #3368, #15375, #251, .T. ) ;
#16851=EDGE_CURVE ( 'NONE', #19704, #9831, #16587, .T. ) ;
#16860=EDGE_LOOP ( 'NONE', ( #11842, #3346, #5881, #17534 ) ) ;
#16876=VECTOR ( 'NONE', #18259, 1000.000000000000000 ) ;
#16894=ORIENTED_EDGE ( 'NONE', *, *, #201, .T. ) ;
#16898=EDGE_LOOP ( 'NONE', ( #17424, #28626, #22660, #19685 ) ) ;
#16913=CARTESIAN_POINT ( 'NONE',  ( -38.11607709268015043, -65.74504297427023403, 1.085364455066277101 ) ) ;
#16986=CARTESIAN_POINT ( 'NONE',  ( -39.50000000000000000, -63.30468293320000583, -2.309401076760000393 ) ) ;
#17027=VERTEX_POINT ( 'NONE', #17221 ) ;
#17040=CARTESIAN_POINT ( 'NONE',  ( -38.25000000000000000, -63.00000000000000000, -1.587713240270000048 ) ) ;
#17102=DIRECTION ( 'NONE',  ( 0.4999999999997570277, 0.000000000000000000, 0.8660254037845789288 ) ) ;
#17112=CARTESIAN_POINT ( 'NONE',  ( -36.79999999999999716, -65.14977478849999670, -0.1732050807570000017 ) ) ;
#17132=DIRECTION ( 'NONE',  ( 0.000000000000000000, -1.000000000000000000, 0.000000000000000000 ) ) ;
#17169=FACE_OUTER_BOUND ( 'NONE', #12755, .T. ) ;
#17182=CARTESIAN_POINT ( 'NONE',  ( -38.25000000000000000, -65.63577453799999262, -1.587713240270000048 ) ) ;
#17193=EDGE_CURVE ( 'NONE', #9831, #5266, #26398, .T. ) ;
#17199=CARTESIAN_POINT ( 'NONE',  ( -42.89961768690000099, -65.31510159580000163, -0.3466308900769999313 ) ) ;
#17217=CARTESIAN_POINT ( 'NONE',  ( -41.70685699858434958, -63.05597747387410834, -2.814055025999628867 ) ) ;
#17221=CARTESIAN_POINT ( 'NONE',  ( -37.75000000000000000, -65.63577453799999262, -0.7216878364849999006 ) ) ;
#17224=B_SPLINE_CURVE_WITH_KNOTS ( 'NONE', 3,
 ( #8461, #1237, #12821, #17217, #21185, #14470, #3677, #3960, #1511, #18991 ),
 .UNSPECIFIED., .F., .F.,
 ( 4, 2, 2, 2, 4 ),
 ( 0.000000000000000000, 0.2500000000000000000, 0.5000000000000000000, 0.7500000000000000000, 1.000000000000000000 ),
 .UNSPECIFIED. ) ;
#17248=ORIENTED_EDGE ( 'NONE', *, *, #23702, .T. ) ;
#17268=AXIS2_PLACEMENT_3D ( 'NONE', #12332, #28349, #27936 ) ;
#17296=AXIS2_PLACEMENT_3D ( 'NONE', #6201, #26318, #20040 ) ;
#17314=PLANE ( 'NONE',  #11274 ) ;
#17328=CARTESIAN_POINT ( 'NONE',  ( -38.25000000000000000, -65.56519245710001087, -1.769653913539999790 ) ) ;
#17381=CARTESIAN_POINT ( 'NONE',  ( -40.28469781717293330, -65.70975255743327637, -2.216737453835613714 ) ) ;
#17385=AXIS2_PLACEMENT_3D ( 'NONE', #28282, #23921, #8314 ) ;
#17414=ORIENTED_EDGE ( 'NONE', *, *, #10853, .T. ) ;
#17424=ORIENTED_EDGE ( 'NONE', *, *, #14512, .T. ) ;
#17450=ORIENTED_EDGE ( 'NONE', *, *, #28485, .F. ) ;
#17478=B_SPLINE_CURVE_WITH_KNOTS ( 'NONE', 5,
 ( #20262, #27125, #7466, #20561, #25083, #9325, #13851, #20719, #18229 ),
 .UNSPECIFIED., .F., .F.,
 ( 6, 3, 6 ),
 ( 0.000000000000000000, 1.237573681330000008, 1.566718891470000097 ),
 .UNSPECIFIED. ) ;
#17482=CARTESIAN_POINT ( 'NONE',  ( -39.50000000000000000, -65.63577453799999262, 2.309401076760000393 ) ) ;
#17501=CARTESIAN_POINT ( 'NONE',  ( -39.77149792059732647, -65.72204893723611008, 2.201677205306737495 ) ) ;
#17502=VERTEX_POINT ( 'NONE', #4501 ) ;
#17534=ORIENTED_EDGE ( 'NONE', *, *, #8341, .F. ) ;
#17540=FACE_OUTER_BOUND ( 'NONE', #13663, .T. ) ;
#17561=EDGE_CURVE ( 'NONE', #14549, #28390, #4771, .T. ) ;
#17577=CARTESIAN_POINT ( 'NONE',  ( -39.83713153847065769, -63.35496709430439921, 2.175426692284139651 ) ) ;
#17600=VERTEX_POINT ( 'NONE', #1747 ) ;
#17605=CARTESIAN_POINT ( 'NONE',  ( -42.51878914953488220, -63.24880261862898578, -0.5665023486488870441 ) ) ;
#17608=CARTESIAN_POINT ( 'NONE',  ( -41.91080743279999865, -63.35440207070000440, -1.043878858150000033 ) ) ;
#17649=CARTESIAN_POINT ( 'NONE',  ( -40.29307695968953595, -65.70763704136885508, 2.219188376449546141 ) ) ;
#17682=CARTESIAN_POINT ( 'NONE',  ( -41.75000000000000000, -65.31510159580000163, 2.337827133090000231 ) ) ;
#17691=CARTESIAN_POINT ( 'NONE',  ( -36.71072769287544446, -65.10052340105973201, 0.07634552798238451732 ) ) ;
#17696=CARTESIAN_POINT ( 'NONE',  ( -38.26484107678280822, -65.11704020643527713, -2.761498650871582416 ) ) ;
#17721=DIRECTION ( 'NONE',  ( 0.000000000000000000, -1.000000000000000000, 0.000000000000000000 ) ) ;
#17756=CARTESIAN_POINT ( 'NONE',  ( -38.25000000000000000, -64.11445222650000630, 2.684678751729999480 ) ) ;
#17769=B_SPLINE_CURVE_WITH_KNOTS ( 'NONE', 3,
 ( #27334, #5335, #6938, #27488 ),
 .UNSPECIFIED., .F., .F.,
 ( 4, 4 ),
 ( 0.000000000000000000, 1.000000000000000000 ),
 .UNSPECIFIED. ) ;
#17784=CARTESIAN_POINT ( 'NONE',  ( -41.75000000000000000, -63.07912966450000880, -2.684678751739999925 ) ) ;
#17805=ADVANCED_FACE ( 'NONE', ( #10394 ), #5898, .T. ) ;
#17818=CARTESIAN_POINT ( 'NONE',  ( -42.04069757566796284, -65.71630940569886548, -0.8827413896567969376 ) ) ;
#17828=CARTESIAN_POINT ( 'NONE',  ( -37.28811165380000148, -65.41419836839999391, -0.4550164754550000135 ) ) ;
#17840=AXIS2_PLACEMENT_3D ( 'NONE', #5340, #11430, #13929 ) ;
#17846=ORIENTED_EDGE ( 'NONE', *, *, #7062, .F. ) ;
#17848=B_SPLINE_CURVE_WITH_KNOTS ( 'NONE', 3,
 ( #15139, #26097, #28271, #3669, #19674, #28144, #17649, #28563, #8598, #26530, #4086, #6125, #21443, #19391, #17501, #8179, #25957, #3810, #21868, #1920 ),
 .UNSPECIFIED., .F., .F.,
 ( 4, 2, 1, 2, 2, 2, 2, 1, 2, 2, 4 ),
 ( 0.000000000000000000, 0.1250000000000256462, 0.1875000000000293099, 0.2187500000000258127, 0.2500000000000223155, 0.5000000000000198730, 0.6250000000000186517, 0.6875000000000109912, 0.7187500000000103251, 0.7500000000000096589, 1.000000000000000000 ),
 .UNSPECIFIED. ) ;
#17856=EDGE_CURVE ( 'NONE', #20440, #3368, #12859, .T. ) ;
#17922=CARTESIAN_POINT ( 'NONE',  ( -39.34243475499999221, -65.56519245710001087, 2.400371413390000264 ) ) ;
#17935=B_SPLINE_CURVE_WITH_KNOTS ( 'NONE', 3,
 ( #19068, #23297, #25769, #23711, #5925, #21121, #12618, #1303, #3342, #1177, #8124, #3754, #20979, #27809, #5797, #7588, #10016, #18930 ),
 .UNSPECIFIED., .F., .F.,
 ( 4, 2, 2, 2, 2, 2, 2, 2, 4 ),
 ( 0.000000000000000000, 0.1249999999999405753, 0.1874999999999341638, 0.2499999999999277800, 0.4999999999999432676, 0.6249999999999517053, 0.6874999999999569233, 0.7499999999999620304, 1.000000000000000000 ),
 .UNSPECIFIED. ) ;
#18068=VERTEX_POINT ( 'NONE', #9952 ) ;
#18076=DIRECTION ( 'NONE',  ( 0.000000000000000000, 1.000000000000000000, 0.000000000000000000 ) ) ;
#18082=VECTOR ( 'NONE', #13818, 1000.000000000000000 ) ;
#18096=DIRECTION ( 'NONE',  ( 0.000000000000000000, -1.000000000000000000, 0.000000000000000000 ) ) ;
#18119=CARTESIAN_POINT ( 'NONE',  ( -37.75000000000000000, -65.63577453799999262, -0.7216878364849999006 ) ) ;
#18164=DIRECTION ( 'NONE',  ( 0.000000000000000000, -1.000000000000000000, 0.000000000000000000 ) ) ;
#18171=DIRECTION ( 'NONE',  ( 0.000000000000000000, 0.000000000000000000, 1.000000000000000000 ) ) ;
#18174=DIRECTION ( 'NONE',  ( 0.000000000000000000, -1.000000000000000000, 0.000000000000000000 ) ) ;
#18192=DIRECTION ( 'NONE',  ( 0.000000000000000000, -1.000000000000000000, 0.000000000000000000 ) ) ;
#18200=CARTESIAN_POINT ( 'NONE',  ( -38.48433347315514652, -65.11310065233233502, 2.895796419436823754 ) ) ;
#18218=EDGE_LOOP ( 'NONE', ( #23879, #19496, #20083, #6939 ) ) ;
#18229=CARTESIAN_POINT ( 'NONE',  ( -41.45000000000000284, -65.14977478849999670, -2.857883832489999776 ) ) ;
#18233=LINE ( 'NONE', #6575, #14832 ) ;
#18234=CARTESIAN_POINT ( 'NONE',  ( -38.02515296818213386, -65.73345158630895924, -0.9555180510348912915 ) ) ;
#18240=DIRECTION ( 'NONE',  ( 0.8775825618903722036, 0.000000000000000000, 0.4794255386042040601 ) ) ;
#18242=ORIENTED_EDGE ( 'NONE', *, *, #2092, .T. ) ;
#18259=DIRECTION ( 'NONE',  ( 0.000000000000000000, -1.000000000000000000, 0.000000000000000000 ) ) ;
#18263=( NAMED_UNIT ( * ) PLANE_ANGLE_UNIT ( ) SI_UNIT ( $, .RADIAN. ) );
#18267=ORIENTED_EDGE ( 'NONE', *, *, #2181, .F. ) ;
#18271=DIRECTION ( 'NONE',  ( 0.000000000000000000, 1.000000000000000000, 0.000000000000000000 ) ) ;
#18279=EDGE_CURVE ( 'NONE', #15375, #20678, #18445, .T. ) ;
#18287=CARTESIAN_POINT ( 'NONE',  ( -40.50000000000000000, -65.00000000000000000, 2.309401076760000393 ) ) ;
#18308=CARTESIAN_POINT ( 'NONE',  ( -38.08919256720000135, -63.35440207070000440, 1.043878858160000034 ) ) ;
#18382=ADVANCED_FACE ( 'NONE', ( #27435 ), #22486, .T. ) ;
#18390=CARTESIAN_POINT ( 'NONE',  ( -41.75000000000000000, -65.14977478849999670, 2.684678751729999480 ) ) ;
#18408=EDGE_LOOP ( 'NONE', ( #3890, #21145, #14547, #4259 ) ) ;
#18409=CARTESIAN_POINT ( 'NONE',  ( -40.00000000000000000, -69.50000000000000000, 0.000000000000000000 ) ) ;
#18425=CARTESIAN_POINT ( 'NONE',  ( -38.06642932020803016, -65.74109364176703707, 1.008752819234915332 ) ) ;
#18427=CARTESIAN_POINT ( 'NONE',  ( -40.00000000000000000, -63.40192378860000133, 0.000000000000000000 ) ) ;
#18445=B_SPLINE_CURVE_WITH_KNOTS ( 'NONE', 5,
 ( #6145, #3686, #21741, #27751, #12550, #21604, #1791, #12830, #21464 ),
 .UNSPECIFIED., .F., .F.,
 ( 6, 3, 6 ),
 ( 0.000000000000000000, 1.237573681330000008, 1.566718891470000097 ),
 .UNSPECIFIED. ) ;
#18478=CARTESIAN_POINT ( 'NONE',  ( -39.12241743810000116, -66.42264973080000345, 0.4794255386039999456 ) ) ;
#18530=ORIENTED_EDGE ( 'NONE', *, *, #22616, .T. ) ;
#18532=CARTESIAN_POINT ( 'NONE',  ( -38.19158192515072869, -63.35070008007209452, -1.239942138225138990 ) ) ;
#18540=CARTESIAN_POINT ( 'NONE',  ( -40.00000000000000000, -63.50000000000000000, 0.000000000000000000 ) ) ;
#18542=( LENGTH_UNIT ( ) NAMED_UNIT ( * ) SI_UNIT ( .MILLI., .METRE. ) );
#18561=CARTESIAN_POINT ( 'NONE',  ( -43.20000000000000284, -65.14977478849999670, 0.1732050807559999961 ) ) ;
#18568=PRODUCT_DEFINITION_FORMATION_WITH_SPECIFIED_SOURCE ( 'ANY', '', #13159, .NOT_KNOWN. ) ;
#18614=EDGE_CURVE ( 'NONE', #8093, #23133, #16000, .T. ) ;
#18624=DIRECTION ( 'NONE',  ( 1.000000000000000000, 0.000000000000000000, 0.000000000000000000 ) ) ;
#18636=AXIS2_PLACEMENT_3D ( 'NONE', #23209, #3528, #12385 ) ;
#18643=DIRECTION ( 'NONE',  ( 0.000000000000000000, -1.000000000000000000, 0.000000000000000000 ) ) ;
#18664=FACE_OUTER_BOUND ( 'NONE', #2312, .T. ) ;
#18680=ORIENTED_EDGE ( 'NONE', *, *, #25228, .F. ) ;
#18686=EDGE_CURVE ( 'NONE', #20283, #14297, #26320, .T. ) ;
#18688=CONICAL_SURFACE ( 'NONE', #22389, 1.732050807582486307, 1.047197551199999799 ) ;
#18694=ORIENTED_EDGE ( 'NONE', *, *, #10109, .F. ) ;
#18721=FACE_OUTER_BOUND ( 'NONE', #26820, .T. ) ;
#18762=VECTOR ( 'NONE', #8799, 1000.000000000000000 ) ;
#18795=LINE ( 'NONE', #7987, #1901 ) ;
#18801=ADVANCED_FACE ( 'NONE', ( #27644 ), #846, .T. ) ;
#18835=AXIS2_PLACEMENT_3D ( 'NONE', #19744, #17721, #15354 ) ;
#18836=EDGE_CURVE ( 'NONE', #20440, #24292, #15976, .T. ) ;
#18895=CARTESIAN_POINT ( 'NONE',  ( -36.05087847149999902, -63.50000000000000000, 2.157414923720000210 ) ) ;
#18910=CARTESIAN_POINT ( 'NONE',  ( -37.75000000000000000, -65.63577453799999262, 0.7216878364859999895 ) ) ;
#18930=CARTESIAN_POINT ( 'NONE',  ( -41.75000000000000000, -65.14977478849999670, -2.684678751739999925 ) ) ;
#18952=CARTESIAN_POINT ( 'NONE',  ( -37.75000000000000000, -65.63577453799999262, -0.7216878364849999006 ) ) ;
#18991=CARTESIAN_POINT ( 'NONE',  ( -41.45000000000000284, -63.07912966450000880, -2.857883832489999776 ) ) ;
#19052=CARTESIAN_POINT ( 'NONE',  ( -41.75000000000000000, -65.21397798589998729, 2.551096136580000007 ) ) ;
#19068=CARTESIAN_POINT ( 'NONE',  ( -41.45000000000000284, -65.14977478849999670, -2.857883832489999776 ) ) ;
#19069=CARTESIAN_POINT ( 'NONE',  ( -41.78768228154088860, -65.71847493511117477, -1.315734964531388718 ) ) ;
#19083=DIRECTION ( 'NONE',  ( 0.000000000000000000, -1.000000000000000000, 0.000000000000000000 ) ) ;
#19179=B_SPLINE_CURVE_WITH_KNOTS ( 'NONE', 3,
 ( #20077, #140, #6826, #15689 ),
 .UNSPECIFIED., .F., .F.,
 ( 4, 4 ),
 ( 0.000000000000000000, 1.000000000000000000 ),
 .UNSPECIFIED. ) ;
#19201=ORIENTED_EDGE ( 'NONE', *, *, #13610, .F. ) ;
#19207=EDGE_CURVE ( 'NONE', #14702, #6476, #12695, .T. ) ;
#19211=CARTESIAN_POINT ( 'NONE',  ( -38.55000000000000426, -63.07912966450000880, 2.857883832489999776 ) ) ;
#19257=ORIENTED_EDGE ( 'NONE', *, *, #25919, .F. ) ;
#19270=B_SPLINE_CURVE_WITH_KNOTS ( 'NONE', 5,
 ( #16152, #9740, #13974, #22879, #14127, #7589, #3076, #22438, #7143 ),
 .UNSPECIFIED., .F., .F.,
 ( 6, 3, 6 ),
 ( 0.000000000000000000, 1.237573681340000009, 1.566718891470000097 ),
 .UNSPECIFIED. ) ;
#19284=CARTESIAN_POINT ( 'NONE',  ( -40.31103002510583622, -65.70299785167240714, -2.224975054963230114 ) ) ;
#19292=CARTESIAN_POINT ( 'NONE',  ( -37.75000000000000000, -63.00000000000000000, 0.7216878364859999895 ) ) ;
#19320=DIRECTION ( 'NONE',  ( 0.000000000000000000, 1.000000000000000000, 0.000000000000000000 ) ) ;
#19323=B_SPLINE_CURVE_WITH_KNOTS ( 'NONE', 3,
 ( #20300, #11693, #665, #9212, #9073, #371, #27017, #11544, #9517, #16211 ),
 .UNSPECIFIED., .F., .F.,
 ( 4, 2, 2, 2, 4 ),
 ( 0.000000000000000000, 0.2500000000000000555, 0.5000000000000000000, 0.7500000000000000000, 1.000000000000000000 ),
 .UNSPECIFIED. ) ;
#19360=FACE_OUTER_BOUND ( 'NONE', #2390, .T. ) ;
#19370=CARTESIAN_POINT ( 'NONE',  ( -38.40529884094686253, -65.09475709727961146, 2.889773311245127374 ) ) ;
#19371=CARTESIAN_POINT ( 'NONE',  ( -38.25000000000000000, -65.21397798589998729, -2.551096136590000008 ) ) ;
#19391=CARTESIAN_POINT ( 'NONE',  ( -39.80530703708314633, -65.72848773095162755, 2.193893542354256709 ) ) ;
#19442=EDGE_CURVE ( 'NONE', #11263, #24995, #1025, .T. ) ;
#19450=CARTESIAN_POINT ( 'NONE',  ( -41.74999999998802025, -63.17171877515596634, -2.272201163158487969 ) ) ;
#19483=CARTESIAN_POINT ( 'NONE',  ( -38.25000000000000000, -63.07912966450000880, 2.684678751729999480 ) ) ;
#19496=ORIENTED_EDGE ( 'NONE', *, *, #12077, .F. ) ;
#19518=ORIENTED_EDGE ( 'NONE', *, *, #23738, .T. ) ;
#19520=CARTESIAN_POINT ( 'NONE',  ( -43.16155280139999917, -65.17124718639999514, -0.1954025812290000053 ) ) ;
#19540=CARTESIAN_POINT ( 'NONE',  ( -38.25000000000000000, -63.17361819573424953, -2.263739386401765863 ) ) ;
#19595=CARTESIAN_POINT ( 'NONE',  ( -38.55000000000000426, -65.14977478849999670, 2.857883832489999776 ) ) ;
#19604=DIRECTION ( 'NONE',  ( 0.000000000000000000, -1.000000000000000000, 0.000000000000000000 ) ) ;
#19605=AXIS2_PLACEMENT_3D ( 'NONE', #15799, #15650, #15200 ) ;
#19613=ORIENTED_EDGE ( 'NONE', *, *, #1371, .T. ) ;
#19618=VERTEX_POINT ( 'NONE', #16689 ) ;
#19633=CARTESIAN_POINT ( 'NONE',  ( -41.75000000000064659, -65.66839995185510759, 1.503614136383694122 ) ) ;
#19650=CARTESIAN_POINT ( 'NONE',  ( -38.25000000000000000, -65.31510159580000163, 2.337827133090000231 ) ) ;
#19655=AXIS2_PLACEMENT_3D ( 'NONE', #11038, #326, #18076 ) ;
#19674=CARTESIAN_POINT ( 'NONE',  ( -40.34155842951303583, -65.69467928435145154, 2.235060801196294467 ) ) ;
#19685=ORIENTED_EDGE ( 'NONE', *, *, #10407, .T. ) ;
#19694=CARTESIAN_POINT ( 'NONE',  ( -36.50000000000000000, -69.00000000000000000, 0.000000000000000000 ) ) ;
#19704=VERTEX_POINT ( 'NONE', #24249 ) ;
#19709=ORIENTED_EDGE ( 'NONE', *, *, #11460, .F. ) ;
#19723=CARTESIAN_POINT ( 'NONE',  ( -36.72197963276312294, -65.10668761694336126, -0.09248738124049776799 ) ) ;
#19744=CARTESIAN_POINT ( 'NONE',  ( -41.54999999999999716, -65.00000000000000000, -2.684678751729999480 ) ) ;
#19749=CARTESIAN_POINT ( 'NONE',  ( -41.70526651914970984, -65.09475709727961146, 2.825938370821126089 ) ) ;
#19762=ORIENTED_EDGE ( 'NONE', *, *, #7877, .T. ) ;
#19764=VECTOR ( 'NONE', #25498, 1000.000000000000000 ) ;
#19791=CARTESIAN_POINT ( 'NONE',  ( -38.25000000000000000, -63.07912966450000880, 2.684678751729999480 ) ) ;
#19792=EDGE_CURVE ( 'NONE', #20678, #14123, #22518, .T. ) ;
#19795=CARTESIAN_POINT ( 'NONE',  ( -38.25000000000000000, -65.19264941160000149, 2.595760183519999931 ) ) ;
#19848=CARTESIAN_POINT ( 'NONE',  ( -41.75000000000000000, -65.49083508809999898, 1.947031612730000028 ) ) ;
#19852=CARTESIAN_POINT ( 'NONE',  ( -43.28961566200059252, -63.05619511567425661, -0.07254510122828666807 ) ) ;
#19857=DIRECTION ( 'NONE',  ( -0.5000000000001882938, 0.000000000000000000, 0.8660254037843299058 ) ) ;
#19986=CARTESIAN_POINT ( 'NONE',  ( -39.57487616197608560, -65.66931566140442555, -2.266171304482763382 ) ) ;
#20001=AXIS2_PLACEMENT_3D ( 'NONE', #24554, #5940, #259 ) ;
#20014=CARTESIAN_POINT ( 'NONE',  ( -38.44108623807613867, -65.10668761693770534, -2.885092602787210136 ) ) ;
#20040=DIRECTION ( 'NONE',  ( -0.8660254037838959196, 0.000000000000000000, 0.5000000000009399148 ) ) ;
#20044=DIRECTION ( 'NONE',  ( 0.8476796612309128731, -0.2588190451029734884, 0.4630895095199519806 ) ) ;
#20077=CARTESIAN_POINT ( 'NONE',  ( -39.50000000000000000, -63.30468293320000583, -2.309401076760000393 ) ) ;
#20079=VERTEX_POINT ( 'NONE', #12212 ) ;
#20083=ORIENTED_EDGE ( 'NONE', *, *, #15529, .F. ) ;
#20091=PLANE ( 'NONE',  #23003 ) ;
#20114=CARTESIAN_POINT ( 'NONE',  ( -40.00000000000000000, -69.00000000000000000, 0.000000000000000000 ) ) ;
#20118=ORIENTED_EDGE ( 'NONE', *, *, #17856, .T. ) ;
#20187=ORIENTED_EDGE ( 'NONE', *, *, #13616, .F. ) ;
#20202=DIRECTION ( 'NONE',  ( 0.8775825618903722036, 0.000000000000000000, 0.4794255386042040601 ) ) ;
#20205=CARTESIAN_POINT ( 'NONE',  ( -37.16454418379386482, -63.17361819572786885, 0.3836747633999084695 ) ) ;
#20230=EDGE_CURVE ( 'NONE', #26111, #21683, #22887, .T. ) ;
#20236=B_SPLINE_CURVE_WITH_KNOTS ( 'NONE', 5,
 ( #28057, #23268, #21498, #23127, #10259, #3175, #7958, #16562, #25598 ),
 .UNSPECIFIED., .F., .F.,
 ( 6, 3, 6 ),
 ( 0.000000000000000000, 1.237573681330000008, 1.566718891470000097 ),
 .UNSPECIFIED. ) ;
#20238=EDGE_CURVE ( 'NONE', #28438, #14549, #10996, .T. ) ;
#20240=CARTESIAN_POINT ( 'NONE',  ( -43.20000000000000284, -63.07912966450000880, 0.1732050807559999961 ) ) ;
#20262=CARTESIAN_POINT ( 'NONE',  ( -40.50000000000000000, -65.63577453799999262, -2.309401076760000393 ) ) ;
#20271=CARTESIAN_POINT ( 'NONE',  ( -37.75000000000000000, -63.30468293320000583, -0.7216878364849999006 ) ) ;
#20281=FACE_BOUND ( 'NONE', #14781, .T. ) ;
#20283=VERTEX_POINT ( 'NONE', #27198 ) ;
#20285=CARTESIAN_POINT ( 'NONE',  ( -42.40756524499999358, -65.56519245710001087, 0.6307174998540000521 ) ) ;
#20290=CARTESIAN_POINT ( 'NONE',  ( -42.25000000000000000, -65.00000000000000000, -0.7216878364880000563 ) ) ;
#20300=CARTESIAN_POINT ( 'NONE',  ( -36.79999999999999716, -63.07912966450000880, -0.1732050807570000017 ) ) ;
#20338=CARTESIAN_POINT ( 'NONE',  ( -41.74999999999999289, -65.11310065233230659, 2.760503925682381343 ) ) ;
#20349=ORIENTED_EDGE ( 'NONE', *, *, #25228, .T. ) ;
#20416=CARTESIAN_POINT ( 'NONE',  ( -38.06767232176576954, -65.74137084432105382, -1.010180990337120832 ) ) ;
#20434=CIRCLE ( 'NONE', #2744, 0.4999999999999985567 ) ;
#20440=VERTEX_POINT ( 'NONE', #24090 ) ;
#20486=CARTESIAN_POINT ( 'NONE',  ( -40.76878914953984179, -63.24880261862722364, -2.464586564602152752 ) ) ;
#20499=CIRCLE ( 'NONE', #13985, 4.999999999999997335 ) ;
#20503=EDGE_CURVE ( 'NONE', #22004, #24058, #8548, .T. ) ;
#20534=EDGE_LOOP ( 'NONE', ( #18694, #15105, #3747, #25692 ) ) ;
#20561=CARTESIAN_POINT ( 'NONE',  ( -40.96188834619999852, -65.41419836839999391, -2.576072437790000169 ) ) ;
#20644=CARTESIAN_POINT ( 'NONE',  ( -38.25000000000000000, -63.30468293320000583, 1.587713240270000048 ) ) ;
#20673=DIRECTION ( 'NONE',  ( 0.000000000000000000, -1.000000000000000000, 0.000000000000000000 ) ) ;
#20678=VERTEX_POINT ( 'NONE', #2985 ) ;
#20689=DIRECTION ( 'NONE',  ( 0.000000000000000000, -1.000000000000000000, 0.000000000000000000 ) ) ;
#20719=CARTESIAN_POINT ( 'NONE',  ( -41.41155280139999917, -65.17124718639999514, -2.835686332019999867 ) ) ;
#20755=CARTESIAN_POINT ( 'NONE',  ( -43.27802036723892343, -65.10668761694192597, 0.09248738125474099958 ) ) ;
#20827=DIRECTION ( 'NONE',  ( 0.000000000000000000, -1.000000000000000000, 0.000000000000000000 ) ) ;
#20849=CARTESIAN_POINT ( 'NONE',  ( -41.45000000000000284, -64.11445222650000630, 2.857883832489999776 ) ) ;
#20896=CARTESIAN_POINT ( 'NONE',  ( -43.28927230711818197, -65.10052340106298630, -0.07634552800406639583 ) ) ;
#20914=LINE ( 'NONE', #18287, #5945 ) ;
#20932=AXIS2_PLACEMENT_3D ( 'NONE', #24126, #24563, #4604 ) ;
#20946=CARTESIAN_POINT ( 'NONE',  ( -40.33874795569358440, -63.33820666351654438, -2.216302165567395122 ) ) ;
#20953=CARTESIAN_POINT ( 'NONE',  ( -42.25000000000000000, -65.00000000000000000, 0.7216878364880000563 ) ) ;
#20979=CARTESIAN_POINT ( 'NONE',  ( -41.70814779298223129, -65.10234783419473104, -2.808123652670708736 ) ) ;
#20991=CARTESIAN_POINT ( 'NONE',  ( -41.75000000000000000, -65.21397798589998729, -2.551096136600000008 ) ) ;
#21040=ORIENTED_EDGE ( 'NONE', *, *, #1489, .F. ) ;
#21069=ORIENTED_EDGE ( 'NONE', *, *, #3181, .T. ) ;
#21087=CARTESIAN_POINT ( 'NONE',  ( -42.25000000000000000, -63.30468293320000583, -0.7216878364880000563 ) ) ;
#21094=AXIS2_PLACEMENT_3D ( 'NONE', #27564, #16470, #14285 ) ;
#21121=CARTESIAN_POINT ( 'NONE',  ( -41.52394852252965762, -65.11704020645255753, -2.883441032528796022 ) ) ;
#21129=DIRECTION ( 'NONE',  ( 0.000000000000000000, -1.000000000000000000, 0.000000000000000000 ) ) ;
#21145=ORIENTED_EDGE ( 'NONE', *, *, #28485, .T. ) ;
#21172=PRESENTATION_STYLE_ASSIGNMENT (( #27735 ) ) ;
#21177=CARTESIAN_POINT ( 'NONE',  ( -43.27242786852578860, -65.10974319587900538, 0.1023444634918562884 ) ) ;
#21185=CARTESIAN_POINT ( 'NONE',  ( -41.68172601867422600, -63.05366291735987971, -2.839252009386262543 ) ) ;
#21186=B_SPLINE_CURVE_WITH_KNOTS ( 'NONE', 3,
 ( #19483, #6082, #12771, #3768, #1459, #8265, #21400, #10300, #7637, #19211 ),
 .UNSPECIFIED., .F., .F.,
 ( 4, 2, 2, 2, 4 ),
 ( 0.000000000000000000, 0.2500000000000000000, 0.5000000000000000000, 0.7500000000000000000, 1.000000000000000000 ),
 .UNSPECIFIED. ) ;
#21221=CARTESIAN_POINT ( 'NONE',  ( -41.51159121739436131, -63.06523941402172539, 2.884620168996051337 ) ) ;
#21222=ORIENTED_EDGE ( 'NONE', *, *, #201, .F. ) ;
#21233=CARTESIAN_POINT ( 'NONE',  ( -38.44999999999999574, -65.00000000000000000, 2.684678751729999480 ) ) ;
#21267=DIRECTION ( 'NONE',  ( 0.000000000000000000, 0.000000000000000000, -1.000000000000000000 ) ) ;
#21270=DIRECTION ( 'NONE',  ( -0.4794255386042028944, 0.000000000000000000, 0.8775825618903727587 ) ) ;
#21274=DIRECTION ( 'NONE',  ( 0.000000000000000000, -1.000000000000000000, 0.000000000000000000 ) ) ;
#21280=ORIENTED_EDGE ( 'NONE', *, *, #23702, .F. ) ;
#21287=COLOUR_RGB ( '', 0.72549020, 0.75294118, 0.79215686) ;
#21383=ORIENTED_EDGE ( 'NONE', *, *, #16847, .F. ) ;
#21385=CIRCLE ( 'NONE', #7921, 4.999999999999997335 ) ;
#21389=CARTESIAN_POINT ( 'NONE',  ( -41.85974496015488455, -65.74398723832253211, -1.129426529332626883 ) ) ;
#21393=PRODUCT_DEFINITION_CONTEXT ( 'detailed design', #14444, 'design' ) ;
#21400=CARTESIAN_POINT ( 'NONE',  ( -38.41801806958173415, -63.05619511567419977, 2.885163282592999145 ) ) ;
#21401=DIRECTION ( 'NONE',  ( 0.000000000000000000, -1.000000000000000000, 0.000000000000000000 ) ) ;
#21407=ORIENTED_EDGE ( 'NONE', *, *, #17193, .F. ) ;
#21411=EDGE_LOOP ( 'NONE', ( #23173, #23694, #22195, #25207 ) ) ;
#21436=VERTEX_POINT ( 'NONE', #28155 ) ;
#21443=CARTESIAN_POINT ( 'NONE',  ( -39.83915519491969803, -65.73344136608082522, 2.187954346637793979 ) ) ;
#21464=CARTESIAN_POINT ( 'NONE',  ( -36.79999999999999716, -65.14977478849999670, 0.1732050807570000017 ) ) ;
#21469=AXIS2_PLACEMENT_3D ( 'NONE', #13334, #4905, #2290 ) ;
#21478=CARTESIAN_POINT ( 'NONE',  ( -40.00000000000000000, -63.00000000000000000, 0.000000000000000000 ) ) ;
#21498=CARTESIAN_POINT ( 'NONE',  ( -40.81117883860000006, -65.49083508809999898, 2.489060262989999828 ) ) ;
#21518=CARTESIAN_POINT ( 'NONE',  ( -39.50000000000000000, -63.30468293320000583, 2.309401076760000393 ) ) ;
#21565=CARTESIAN_POINT ( 'NONE',  ( -38.25000000000000000, -65.21397798589998729, 2.551096136590000008 ) ) ;
#21570=AXIS2_PLACEMENT_3D ( 'NONE', #3862, #28191, #25355 ) ;
#21595=EDGE_LOOP ( 'NONE', ( #2233, #6731, #3296, #17248 ) ) ;
#21604=CARTESIAN_POINT ( 'NONE',  ( -36.91568593819999933, -65.21397798589998729, 0.2399963883279999932 ) ) ;
#21611=AXIS2_PLACEMENT_3D ( 'NONE', #11703, #8063, #23646 ) ;
#21612=CARTESIAN_POINT ( 'NONE',  ( -39.77168464789694724, -65.72207046437310396, -2.201769106273790744 ) ) ;
#21634=DIRECTION ( 'NONE',  ( -0.4794255386042028944, 0.000000000000000000, 0.8775825618903727587 ) ) ;
#21673=AXIS2_PLACEMENT_3D ( 'NONE', #12102, #9918, #9777 ) ;
#21676=ORIENTED_EDGE ( 'NONE', *, *, #7329, .F. ) ;
#21683=VERTEX_POINT ( 'NONE', #1209 ) ;
#21687=CARTESIAN_POINT ( 'NONE',  ( -41.99080665327601736, -63.35144866726079016, -0.9204318062483302088 ) ) ;
#21694=FACE_OUTER_BOUND ( 'NONE', #3595, .T. ) ;
#21741=CARTESIAN_POINT ( 'NONE',  ( -37.43882116139999994, -65.49083508809999898, 0.5420286502519999772 ) ) ;
#21790=PLANE ( 'NONE',  #17296 ) ;
#21792=FACE_OUTER_BOUND ( 'NONE', #10554, .T. ) ;
#21803=ADVANCED_FACE ( 'NONE', ( #27426 ), #14570, .F. ) ;
#21868=CARTESIAN_POINT ( 'NONE',  ( -39.57283196047948337, -65.66839995188320245, 2.267351524782069472 ) ) ;
#21895=CARTESIAN_POINT ( 'NONE',  ( -42.25000000000000000, -65.63577453799999262, -0.7216878364880000563 ) ) ;
#21916=EDGE_CURVE ( 'NONE', #19618, #5266, #5425, .T. ) ;
#21937=VERTEX_POINT ( 'NONE', #12646 ) ;
#21963=VECTOR ( 'NONE', #27628, 1000.000000000000000 ) ;
#21974=CARTESIAN_POINT ( 'NONE',  ( -41.98619589785989348, -65.73347097107149750, 0.9353054002211724782 ) ) ;
#21977=ORIENTED_EDGE ( 'NONE', *, *, #15529, .T. ) ;
#22004=VERTEX_POINT ( 'NONE', #20240 ) ;
#22033=B_SPLINE_CURVE_WITH_KNOTS ( 'NONE', 3,
 ( #25666, #16913, #16344, #27722, #25252, #936, #5421, #7762, #7628, #16491, #25395, #5559 ),
 .UNSPECIFIED., .F., .F.,
 ( 4, 2, 1, 1, 2, 2, 4 ),
 ( 0.000000000000000000, 0.2500000000000220934, 0.3750000000000266454, 0.4375000000000288658, 0.4687500000000406342, 0.5000000000000524025, 1.000000000000000000 ),
 .UNSPECIFIED. ) ;
#22047=CARTESIAN_POINT ( 'NONE',  ( -42.05565522495096076, -65.71171110559873796, -0.8680096503517884532 ) ) ;
#22063=CARTESIAN_POINT ( 'NONE',  ( -43.29971333826889435, -63.05366661935828176, -0.03681143521561272558 ) ) ;
#22066=DIRECTION ( 'NONE',  ( 0.000000000000000000, -1.000000000000000000, 0.000000000000000000 ) ) ;
#22124=ORIENTED_EDGE ( 'NONE', *, *, #19792, .T. ) ;
#22132=CARTESIAN_POINT ( 'NONE',  ( -41.75000000000000000, -63.30468293320000583, -1.587713240270000048 ) ) ;
#22155=CARTESIAN_POINT ( 'NONE',  ( -43.20000000000000284, -65.14977478849999670, -0.1732050807570000017 ) ) ;
#22176=DIRECTION ( 'NONE',  ( 0.000000000000000000, -1.000000000000000000, 0.000000000000000000 ) ) ;
#22182=EDGE_CURVE ( 'NONE', #26536, #20079, #6765, .T. ) ;
#22195=ORIENTED_EDGE ( 'NONE', *, *, #19792, .F. ) ;
#22223=DIRECTION ( 'NONE',  ( 0.000000000000000000, 0.000000000000000000, -1.000000000000000000 ) ) ;
#22227=CYLINDRICAL_SURFACE ( 'NONE', #4742, 2.999999999999998668 ) ;
#22232=LINE ( 'NONE', #10975, #27530 ) ;
#22254=VERTEX_POINT ( 'NONE', #22988 ) ;
#22311=CARTESIAN_POINT ( 'NONE',  ( -42.25000000000000000, -63.00000000000000000, -0.7216878364880000563 ) ) ;
#22329=B_SPLINE_CURVE_WITH_KNOTS ( 'NONE', 5,
 ( #27260, #9611, #2643, #13840, #4957, #20991, #11491, #23036, #25071 ),
 .UNSPECIFIED., .F., .F.,
 ( 6, 3, 6 ),
 ( 0.000000000000000000, 1.237573681350000010, 1.566718891480000098 ),
 .UNSPECIFIED. ) ;
#22330=ADVANCED_FACE ( 'NONE', ( #13419 ), #22433, .F. ) ;
#22359=CARTESIAN_POINT ( 'NONE',  ( -38.31563671849563235, -65.09473604208548636, -2.838061730473900202 ) ) ;
#22389=AXIS2_PLACEMENT_3D ( 'NONE', #22793, #18271, #2833 ) ;
#22398=CIRCLE ( 'NONE', #17268, 3.500000000000003109 ) ;
#22403=ORIENTED_EDGE ( 'NONE', *, *, #26083, .F. ) ;
#22408=CIRCLE ( 'NONE', #19605, 3.000000000000002665 ) ;
#22433=CONICAL_SURFACE ( 'NONE', #27098, 1.732050807582486307, 1.047197551199999799 ) ;
#22438=CARTESIAN_POINT ( 'NONE',  ( -38.58844719860000083, -65.17124718639999514, -2.835686332019999867 ) ) ;
#22450=ORIENTED_EDGE ( 'NONE', *, *, #22182, .F. ) ;
#22456=PLANE ( 'NONE',  #19655 ) ;
#22465=PLANE ( 'NONE',  #14482 ) ;
#22468=CARTESIAN_POINT ( 'NONE',  ( -38.25000000001038103, -63.32098044081165256, -1.497193467875711503 ) ) ;
#22471=VERTEX_POINT ( 'NONE', #26700 ) ;
#22486=TOROIDAL_SURFACE ( 'NONE', #25748, 4.500000000000000000, 0.5000000000000000000 ) ;
#22491=LINE ( 'NONE', #20290, #16876 ) ;
#22492=EDGE_CURVE ( 'NONE', #3368, #2835, #22033, .T. ) ;
#22510=CARTESIAN_POINT ( 'NONE',  ( -37.94434432234054810, -65.71171096279377366, 0.8680092137352279913 ) ) ;
#22518=B_SPLINE_CURVE_WITH_KNOTS ( 'NONE', 3,
 ( #8780, #28468, #1971, #8504, #26300, #15482, #11257, #17691, #15182, #26437, #24096, #24392, #10814, #19723, #28611, #8642, #6466, #26579 ),
 .UNSPECIFIED., .F., .F.,
 ( 4, 2, 2, 2, 2, 2, 2, 2, 4 ),
 ( 0.000000000000000000, 0.1249999999999761302, 0.1874999999999816536, 0.2499999999999872324, 0.5000000000000115463, 0.6250000000000236478, 0.6875000000000296430, 0.7500000000000357492, 1.000000000000000000 ),
 .UNSPECIFIED. ) ;
#22533=DIRECTION ( 'NONE',  ( 0.000000000000000000, -1.000000000000000000, 0.000000000000000000 ) ) ;
#22603=ORIENTED_EDGE ( 'NONE', *, *, #2048, .T. ) ;
#22616=EDGE_CURVE ( 'NONE', #2835, #27862, #23784, .T. ) ;
#22632=CARTESIAN_POINT ( 'NONE',  ( -43.12299426110000411, -65.19264941160000149, 0.2176643648609999926 ) ) ;
#22646=LINE ( 'NONE', #25275, #7959 ) ;
#22660=ORIENTED_EDGE ( 'NONE', *, *, #1721, .F. ) ;
#22669=CARTESIAN_POINT ( 'NONE',  ( -38.08919256720000135, -63.35440207070000440, 1.043878858160000034 ) ) ;
#22679=B_SPLINE_CURVE_WITH_KNOTS ( 'NONE', 3,
 ( #28103, #5813, #25645, #1600, #5674, #28377 ),
 .UNSPECIFIED., .F., .F.,
 ( 4, 2, 4 ),
 ( 0.000000000000000000, 0.5000000000000002220, 1.000000000000000000 ),
 .UNSPECIFIED. ) ;
#22761=AXIS2_PLACEMENT_3D ( 'NONE', #15471, #24379, #4422 ) ;
#22773=( NAMED_UNIT ( * ) PLANE_ANGLE_UNIT ( ) SI_UNIT ( $, .RADIAN. ) );
#22793=CARTESIAN_POINT ( 'NONE',  ( -40.00000000000000000, -66.00000000000000000, 0.000000000000000000 ) ) ;
#22857=EDGE_LOOP ( 'NONE', ( #156, #20118, #3598, #6825, #22124, #12852, #23855, #24227, #10615, #17450, #10998, #230, #28778, #23134, #23546, #6329 ) ) ;
#22877=EDGE_CURVE ( 'NONE', #22004, #25894, #3008, .T. ) ;
#22879=CARTESIAN_POINT ( 'NONE',  ( -39.03811165380000148, -65.41419836839999391, -2.576072437790000169 ) ) ;
#22887=B_SPLINE_CURVE_WITH_KNOTS ( 'NONE', 3,
 ( #109, #20486, #2582, #13928 ),
 .UNSPECIFIED., .F., .F.,
 ( 4, 4 ),
 ( 0.000000000000000000, 1.000000000000000000 ),
 .UNSPECIFIED. ) ;
#22888=PRODUCT_CONTEXT ( 'NONE', #15339, 'mechanical' ) ;
#22908=ORIENTED_EDGE ( 'NONE', *, *, #21916, .F. ) ;
#22968=CIRCLE ( 'NONE', #24824, 3.500000000000003109 ) ;
#22971=ORIENTED_EDGE ( 'NONE', *, *, #10407, .F. ) ;
#22988=CARTESIAN_POINT ( 'NONE',  ( -42.25000000000000000, -65.63577453799999262, 0.7216878364880000563 ) ) ;
#23003=AXIS2_PLACEMENT_3D ( 'NONE', #27240, #27099, #20689 ) ;
#23023=EDGE_CURVE ( 'NONE', #22254, #25894, #16824, .T. ) ;
#23036=CARTESIAN_POINT ( 'NONE',  ( -41.75000000000000000, -65.17124718639999514, -2.640283750799999662 ) ) ;
#23042=DIRECTION ( 'NONE',  ( 0.000000000000000000, -1.000000000000000000, 0.000000000000000000 ) ) ;
#23127=CARTESIAN_POINT ( 'NONE',  ( -40.96188834619999852, -65.41419836839999391, 2.576072437790000169 ) ) ;
#23133=VERTEX_POINT ( 'NONE', #19595 ) ;
#23134=ORIENTED_EDGE ( 'NONE', *, *, #1249, .F. ) ;
#23139=ORIENTED_EDGE ( 'NONE', *, *, #20238, .F. ) ;
#23173=ORIENTED_EDGE ( 'NONE', *, *, #26651, .F. ) ;
#23209=CARTESIAN_POINT ( 'NONE',  ( -43.20000000000000284, -63.00000000000000000, 0.1732050807559999961 ) ) ;
#23210=ORIENTED_EDGE ( 'NONE', *, *, #5241, .F. ) ;
#23212=AXIS2_PLACEMENT_3D ( 'NONE', #748, #20827, #7721 ) ;
#23213=EDGE_CURVE ( 'NONE', #14549, #2835, #3733, .T. ) ;
#23266=CARTESIAN_POINT ( 'NONE',  ( -41.45000000000000284, -65.14977478849999670, -2.857883832489999776 ) ) ;
#23268=CARTESIAN_POINT ( 'NONE',  ( -40.65756524500000069, -65.56519245710001087, 2.400371413390000264 ) ) ;
#23269=ORIENTED_EDGE ( 'NONE', *, *, #19442, .T. ) ;
#23292=ORIENTED_EDGE ( 'NONE', *, *, #20503, .T. ) ;
#23297=CARTESIAN_POINT ( 'NONE',  ( -41.46399166428601291, -65.14196057592134537, -2.865961923652742271 ) ) ;
#23338=EDGE_CURVE ( 'NONE', #5567, #6872, #22491, .T. ) ;
#23357=CARTESIAN_POINT ( 'NONE',  ( -43.28598031665701740, -65.10234783420354177, 0.07523755578869117944 ) ) ;
#23394=ADVANCED_FACE ( 'NONE', ( #13547 ), #22456, .T. ) ;
#23446=CARTESIAN_POINT ( 'NONE',  ( -41.78982036957599888, -65.72001381778289897, -1.308254260903399357 ) ) ;
#23468=EDGE_CURVE ( 'NONE', #8977, #21937, #23847, .T. ) ;
#23488=CARTESIAN_POINT ( 'NONE',  ( -35.61208719050000582, -69.00000000000000000, 2.397127693020000283 ) ) ;
#23496=ADVANCED_FACE ( 'NONE', ( #19360 ), #17314, .T. ) ;
#23507=DIRECTION ( 'NONE',  ( 1.000000000000000000, 0.000000000000000000, 0.000000000000000000 ) ) ;
#23544=CARTESIAN_POINT ( 'NONE',  ( -41.75000000000000000, -63.07912966450000880, 2.684678751729999480 ) ) ;
#23546=ORIENTED_EDGE ( 'NONE', *, *, #28542, .F. ) ;
#23548=CARTESIAN_POINT ( 'NONE',  ( -42.75000000000000000, -65.00000000000000000, -1.587713240270000048 ) ) ;
#23569=DIRECTION ( 'NONE',  ( 0.000000000000000000, -1.000000000000000000, 0.000000000000000000 ) ) ;
#23595=FACE_OUTER_BOUND ( 'NONE', #1370, .T. ) ;
#23646=DIRECTION ( 'NONE',  ( 1.000000000000000000, 0.000000000000000000, 0.000000000000000000 ) ) ;
#23664=B_SPLINE_CURVE_WITH_KNOTS ( 'NONE', 3,
 ( #27424, #22468, #3104, #18532, #339, #13859, #16182, #26987, #9041, #20271 ),
 .UNSPECIFIED., .F., .F.,
 ( 4, 2, 2, 2, 4 ),
 ( 0.000000000000000000, 0.2500000000000000000, 0.5000000000000000000, 0.7500000000000000000, 1.000000000000000000 ),
 .UNSPECIFIED. ) ;
#23694=ORIENTED_EDGE ( 'NONE', *, *, #15300, .T. ) ;
#23701=CARTESIAN_POINT ( 'NONE',  ( -40.16286586133305292, -63.35496135697056275, 2.175426268797550744 ) ) ;
#23702=EDGE_CURVE ( 'NONE', #5567, #24058, #4937, .T. ) ;
#23711=CARTESIAN_POINT ( 'NONE',  ( -41.50091764415566331, -65.12549727761340534, -2.878985763018412136 ) ) ;
#23712=CARTESIAN_POINT ( 'NONE',  ( -41.76385502083800105, -65.70026997502756672, -1.401764440866061667 ) ) ;
#23738=EDGE_CURVE ( 'NONE', #790, #19618, #25192, .T. ) ;
#23741=B_SPLINE_CURVE_WITH_KNOTS ( 'NONE', 3,
 ( #22669, #27189, #16093, #12422 ),
 .UNSPECIFIED., .F., .F.,
 ( 4, 4 ),
 ( 0.000000000000000000, 1.000000000000000000 ),
 .UNSPECIFIED. ) ;
#23754=ADVANCED_BREP_SHAPE_REPRESENTATION ( '', ( #16071, #26433 ), #5492 ) ;
#23761=EDGE_LOOP ( 'NONE', ( #10582, #22908, #7707, #4098 ) ) ;
#23784=B_SPLINE_CURVE_WITH_KNOTS ( 'NONE', 5,
 ( #12931, #10885, #15116, #1898, #19650, #21565, #19795, #14981, #15257 ),
 .UNSPECIFIED., .F., .F.,
 ( 6, 3, 6 ),
 ( 0.000000000000000000, 1.237573681330000008, 1.566718891470000097 ),
 .UNSPECIFIED. ) ;
#23798=AXIS2_PLACEMENT_3D ( 'NONE', #4612, #18164, #20202 ) ;
#23847=CIRCLE ( 'NONE', #21094, 4.999999999999997335 ) ;
#23855=ORIENTED_EDGE ( 'NONE', *, *, #26895, .F. ) ;
#23869=CARTESIAN_POINT ( 'NONE',  ( -35.50000000000000000, -63.00000000000000000, 0.000000000000000000 ) ) ;
#23876=CARTESIAN_POINT ( 'NONE',  ( -42.52792552673321325, -63.24690319806013150, 0.5612274588118402185 ) ) ;
#23879=ORIENTED_EDGE ( 'NONE', *, *, #1489, .T. ) ;
#23880=CARTESIAN_POINT ( 'NONE',  ( -40.00000000000000000, -66.00000000000000000, 0.000000000000000000 ) ) ;
#23894=CARTESIAN_POINT ( 'NONE',  ( -39.18882116139999994, -65.49083508809999898, 2.489060262989999828 ) ) ;
#23921=DIRECTION ( 'NONE',  ( 0.000000000000000000, -1.000000000000000000, 0.000000000000000000 ) ) ;
#24003=EDGE_CURVE ( 'NONE', #24292, #22471, #14593, .T. ) ;
#24010=CARTESIAN_POINT ( 'NONE',  ( -42.10639864760541684, -65.69467928435254578, 0.8217321237320240890 ) ) ;
#24018=DIRECTION ( 'NONE',  ( 0.000000000000000000, 1.000000000000000000, 0.000000000000000000 ) ) ;
#24020=CARTESIAN_POINT ( 'NONE',  ( -37.75000000000000000, -63.30468293320000583, -0.7216878364849999006 ) ) ;
#24058=VERTEX_POINT ( 'NONE', #8450 ) ;
#24080=FACE_OUTER_BOUND ( 'NONE', #4832, .T. ) ;
#24089=DIRECTION ( 'NONE',  ( 0.8775825618903723147, 0.000000000000000000, 0.4794255386042037825 ) ) ;
#24090=CARTESIAN_POINT ( 'NONE',  ( -38.24483487620000233, -65.84529946160000691, 0.9588510772079998912 ) ) ;
#24096=CARTESIAN_POINT ( 'NONE',  ( -36.70269827918048122, -65.09619745167545091, -0.03908829155573841085 ) ) ;
#24126=CARTESIAN_POINT ( 'NONE',  ( -40.00000000000000000, -63.50000000000000000, 0.000000000000000000 ) ) ;
#24133=EDGE_CURVE ( 'NONE', #20283, #17502, #22968, .T. ) ;
#24147=CONICAL_SURFACE ( 'NONE', #11575, 1.732050807582486307, 1.047197551199999799 ) ;
#24176=CARTESIAN_POINT ( 'NONE',  ( -38.08919256720000135, -63.35440207070000440, 1.043878858160000034 ) ) ;
#24190=CARTESIAN_POINT ( 'NONE',  ( -42.40756524499999358, -65.56519245710001087, -0.6307174998540000521 ) ) ;
#24213=EDGE_CURVE ( 'NONE', #1763, #10539, #9784, .T. ) ;
#24227=ORIENTED_EDGE ( 'NONE', *, *, #21916, .T. ) ;
#24231=VECTOR ( 'NONE', #21274, 1000.000000000000000 ) ;
#24242=CARTESIAN_POINT ( 'NONE',  ( -43.20000000000000284, -63.07912966450000880, 0.1732050807559999961 ) ) ;
#24249=CARTESIAN_POINT ( 'NONE',  ( -38.55000000000000426, -63.07912966450000880, -2.857883832489999776 ) ) ;
#24266=DIRECTION ( 'NONE',  ( 0.5000000000001882938, 0.000000000000000000, -0.8660254037843299058 ) ) ;
#24273=CARTESIAN_POINT ( 'NONE',  ( -39.50000000000000000, -65.63577453799999262, 2.309401076760000393 ) ) ;
#24283=CARTESIAN_POINT ( 'NONE',  ( -37.48121085046030743, -63.24880261862786313, 0.5665023486436212563 ) ) ;
#24284=ORIENTED_EDGE ( 'NONE', *, *, #26651, .T. ) ;
#24292=VERTEX_POINT ( 'NONE', #16753 ) ;
#24339=PRODUCT_DEFINITION_SHAPE ( 'NONE', 'NONE',  #121 ) ;
#24343=DIRECTION ( 'NONE',  ( 1.000000000000000000, 0.000000000000000000, 0.000000000000000000 ) ) ;
#24368=CARTESIAN_POINT ( 'NONE',  ( -39.65151520464630153, -65.69483747912252625, -2.234885500246811763 ) ) ;
#24379=DIRECTION ( 'NONE',  ( 0.000000000000000000, -1.000000000000000000, 0.000000000000000000 ) ) ;
#24392=CARTESIAN_POINT ( 'NONE',  ( -36.71069433210978872, -65.10053925468626801, -0.06637106436662004727 ) ) ;
#24395=CARTESIAN_POINT ( 'NONE',  ( -41.91080743279999865, -63.35440207070000440, -1.043878858150000033 ) ) ;
#24428=CARTESIAN_POINT ( 'NONE',  ( -38.55000000000000426, -63.07912966450000880, 2.857883832489999776 ) ) ;
#24434=EDGE_CURVE ( 'NONE', #28363, #22004, #12544, .T. ) ;
#24450=CARTESIAN_POINT ( 'NONE',  ( -42.25000000000000000, -65.63577453799999262, 0.7216878364880000563 ) ) ;
#24453=CARTESIAN_POINT ( 'NONE',  ( -42.10477055614926911, -63.33487562142746441, -0.8055360949872770737 ) ) ;
#24505=EDGE_CURVE ( 'NONE', #4023, #17027, #6682, .T. ) ;
#24515=DIRECTION ( 'NONE',  ( 0.000000000000000000, -1.000000000000000000, 0.000000000000000000 ) ) ;
#24523=CARTESIAN_POINT ( 'NONE',  ( -36.83844719860000083, -65.17124718639999514, -0.1954025812290000053 ) ) ;
#24540=EDGE_CURVE ( 'NONE', #28390, #27862, #15548, .T. ) ;
#24554=CARTESIAN_POINT ( 'NONE',  ( -40.00000000000000000, -94.00000000000000000, 0.000000000000000000 ) ) ;
#24563=DIRECTION ( 'NONE',  ( 0.000000000000000000, -1.000000000000000000, 0.000000000000000000 ) ) ;
#24591=ORIENTED_EDGE ( 'NONE', *, *, #6428, .F. ) ;
#24690=SHAPE_REPRESENTATION ( 'Housing Torx Attachment Screw', ( #26433 ), #5492 ) ;
#24714=ORIENTED_EDGE ( 'NONE', *, *, #938, .T. ) ;
#24717=CARTESIAN_POINT ( 'NONE',  ( -38.17962778057142970, -63.35319846927643539, 1.206297397038823771 ) ) ;
#24752=EDGE_CURVE ( 'NONE', #790, #9831, #14634, .T. ) ;
#24796=DIRECTION ( 'NONE',  ( 0.000000000000000000, -1.000000000000000000, 0.000000000000000000 ) ) ;
#24797=CARTESIAN_POINT ( 'NONE',  ( -38.22437212383332650, -65.70788121357088585, -1.362554289316070477 ) ) ;
#24824=AXIS2_PLACEMENT_3D ( 'NONE', #26833, #4671, #26979 ) ;
#24836=CARTESIAN_POINT ( 'NONE',  ( -38.24999999999320011, -65.14196057591033195, -2.700834934057557479 ) ) ;
#24853=CARTESIAN_POINT ( 'NONE',  ( -39.50000000000000000, -65.63577453799999262, -2.309401076760000393 ) ) ;
#24885=ADVANCED_FACE ( 'NONE', ( #26692 ), #11215, .T. ) ;
#24888=ORIENTED_EDGE ( 'NONE', *, *, #18836, .T. ) ;
#24896=VECTOR ( 'NONE', #22176, 1000.000000000000000 ) ;
#24941=CARTESIAN_POINT ( 'NONE',  ( -37.96285680772825089, -65.71745250376275749, -0.8863062584507671593 ) ) ;
#24967=CARTESIAN_POINT ( 'NONE',  ( -37.10038231309999901, -65.31510159580000163, -0.3466308900760000089 ) ) ;
#24995=VERTEX_POINT ( 'NONE', #18390 ) ;
#25014=EDGE_CURVE ( 'NONE', #790, #4023, #23664, .T. ) ;
#25028=DIRECTION ( 'NONE',  ( 0.000000000000000000, -1.000000000000000000, 0.000000000000000000 ) ) ;
#25034=ORIENTED_EDGE ( 'NONE', *, *, #26610, .F. ) ;
#25071=CARTESIAN_POINT ( 'NONE',  ( -41.75000000000000000, -65.14977478849999670, -2.684678751739999925 ) ) ;
#25083=CARTESIAN_POINT ( 'NONE',  ( -41.14961768690000099, -65.31510159580000163, -2.684458023169999930 ) ) ;
#25085=ORIENTED_EDGE ( 'NONE', *, *, #26924, .F. ) ;
#25117=SURFACE_STYLE_FILL_AREA ( #5298 ) ;
#25134=CARTESIAN_POINT ( 'NONE',  ( -38.51943391351900914, -63.07120704560256996, -2.875531170737058773 ) ) ;
#25137=CARTESIAN_POINT ( 'NONE',  ( -43.94912152850000098, -63.00000000000000000, -2.157414923720000210 ) ) ;
#25192=LINE ( 'NONE', #27082, #5284 ) ;
#25207=ORIENTED_EDGE ( 'NONE', *, *, #2092, .F. ) ;
#25228=EDGE_CURVE ( 'NONE', #27862, #23133, #13913, .T. ) ;
#25252=CARTESIAN_POINT ( 'NONE',  ( -38.18612978632862820, -65.73322674265560295, 1.234409484183223604 ) ) ;
#25255=DIRECTION ( 'NONE',  ( 1.000000000000000000, 0.000000000000000000, 0.000000000000000000 ) ) ;
#25258=ADVANCED_FACE ( 'NONE', ( #11776 ), #20091, .T. ) ;
#25262=FACE_OUTER_BOUND ( 'NONE', #27927, .T. ) ;
#25275=CARTESIAN_POINT ( 'NONE',  ( -42.63274768570000361, -81.75000000000000000, -1.438276615809999992 ) ) ;
#25278=ORIENTED_EDGE ( 'NONE', *, *, #13066, .F. ) ;
#25350=VECTOR ( 'NONE', #11284, 1000.000000000000000 ) ;
#25355=DIRECTION ( 'NONE',  ( -1.000000000000000000, 0.000000000000000000, 6.505213034913020688E-16 ) ) ;
#25356=CARTESIAN_POINT ( 'NONE',  ( -40.50000000000000000, -63.30468293320000583, -2.309401076760000393 ) ) ;
#25367=EDGE_LOOP ( 'NONE', ( #26780, #10057, #14283, #8488, #16293, #9568, #27263, #14688, #9890, #22603, #24284, #22450, #7696, #2743, #8157, #2896 ) ) ;
#25395=CARTESIAN_POINT ( 'NONE',  ( -38.25000000000000711, -65.67306013599088033, 1.491601497604051918 ) ) ;
#25404=CARTESIAN_POINT ( 'NONE',  ( -41.75000000000000000, -63.30468293320000583, 1.587713240270000048 ) ) ;
#25410=CARTESIAN_POINT ( 'NONE',  ( -43.25910744576837175, -65.11704020644228308, -0.1219423816561529955 ) ) ;
#25420=CARTESIAN_POINT ( 'NONE',  ( -37.81585169939486946, -65.66527311162126068, 0.7597073328712810047 ) ) ;
#25429=CARTESIAN_POINT ( 'NONE',  ( -35.61208719050000582, -66.25000000000000000, 2.397127693020000283 ) ) ;
#25473=VERTEX_POINT ( 'NONE', #7248 ) ;
#25491=UNCERTAINTY_MEASURE_WITH_UNIT (LENGTH_MEASURE( 1.000000000000000082E-05 ), #18542, 'distance_accuracy_value', 'NONE');
#25498=DIRECTION ( 'NONE',  ( 0.7600087925152557711, -0.5000000000001688649, 0.4151946956541399114 ) ) ;
#25542=CARTESIAN_POINT ( 'NONE',  ( -43.26282332285115473, -65.11500191527875359, -0.1170746919366537492 ) ) ;
#25548=CARTESIAN_POINT ( 'NONE',  ( -42.75000000000000000, -65.00000000000000000, 1.587713240270000048 ) ) ;
#25555=CARTESIAN_POINT ( 'NONE',  ( -38.55000000000000426, -65.14977478849999670, -2.857883832489999776 ) ) ;
#25598=CARTESIAN_POINT ( 'NONE',  ( -41.45000000000000284, -65.14977478849999670, 2.857883832489999776 ) ) ;
#25606=EDGE_CURVE ( 'NONE', #25473, #10539, #15262, .T. ) ;
#25610=VERTEX_POINT ( 'NONE', #23266 ) ;
#25614=CARTESIAN_POINT ( 'NONE',  ( -41.75000000000000000, -65.17124718639999514, 2.640283750780000105 ) ) ;
#25645=CARTESIAN_POINT ( 'NONE',  ( -41.96540734349659374, -63.35496135697054854, 0.9466671610960367689 ) ) ;
#25649=CARTESIAN_POINT ( 'NONE',  ( -43.07153896660000214, -69.50000000000000000, -1.677989385109999843 ) ) ;
#25666=CARTESIAN_POINT ( 'NONE',  ( -38.08919256720000135, -65.74290439030001210, 1.043878858160000034 ) ) ;
#25692=ORIENTED_EDGE ( 'NONE', *, *, #14208, .F. ) ;
#25744=LINE ( 'NONE', #5633, #3251 ) ;
#25748=AXIS2_PLACEMENT_3D ( 'NONE', #18540, #18096, #4982 ) ;
#25751=CARTESIAN_POINT ( 'NONE',  ( -40.50000000000000000, -63.30468293320000583, 2.309401076760000393 ) ) ;
#25769=CARTESIAN_POINT ( 'NONE',  ( -41.47847536571098459, -65.13491442162823830, -2.872258511071608567 ) ) ;
#25779=CARTESIAN_POINT ( 'NONE',  ( -36.05087847149999902, -63.00000000000000000, 2.157414923720000210 ) ) ;
#25780=CARTESIAN_POINT ( 'NONE',  ( -40.87758256189999884, -66.42264973080000345, -0.4794255386039999456 ) ) ;
#25817=CARTESIAN_POINT ( 'NONE',  ( -37.58664795480000009, -63.20096189429999356, 1.318420231159999956 ) ) ;
#25860=VERTEX_POINT ( 'NONE', #25137 ) ;
#25894=VERTEX_POINT ( 'NONE', #5167 ) ;
#25915=ORIENTED_EDGE ( 'NONE', *, *, #14756, .F. ) ;
#25919=EDGE_CURVE ( 'NONE', #2354, #26414, #26740, .T. ) ;
#25922=CARTESIAN_POINT ( 'NONE',  ( -38.55000000000000426, -65.14977478849999670, -2.857883832489999776 ) ) ;
#25945=ORIENTED_EDGE ( 'NONE', *, *, #25014, .F. ) ;
#25948=CARTESIAN_POINT ( 'NONE',  ( -43.07153896660000214, -69.00000000000000000, -1.677989385109999843 ) ) ;
#25957=CARTESIAN_POINT ( 'NONE',  ( -39.73620294722308444, -65.71460843033641197, 2.210699957725660525 ) ) ;
#26036=ORIENTED_EDGE ( 'NONE', *, *, #15300, .F. ) ;
#26069=CARTESIAN_POINT ( 'NONE',  ( -38.25000000000000000, -65.19264941160000149, -2.595760183519999931 ) ) ;
#26083=EDGE_CURVE ( 'NONE', #26536, #15375, #18795, .T. ) ;
#26088=CARTESIAN_POINT ( 'NONE',  ( -43.08431406180000067, -65.21397798589998729, -0.2399963883299999767 ) ) ;
#26097=CARTESIAN_POINT ( 'NONE',  ( -40.46358016753210052, -65.65208897057550530, 2.288374076695098402 ) ) ;
#26111=VERTEX_POINT ( 'NONE', #25356 ) ;
#26153=B_SPLINE_CURVE_WITH_KNOTS ( 'NONE', 3,
 ( #1524, #10368, #1798, #10642, #8480, #19284, #28169, #17381, #6008, #14887, #1665, #26275, #6297, #12698, #21612, #15162, #11233, #24368, #19986, #15758 ),
 .UNSPECIFIED., .F., .F.,
 ( 4, 2, 1, 2, 2, 2, 2, 1, 2, 2, 4 ),
 ( 0.000000000000000000, 0.1249999999999719114, 0.1874999999999518996, 0.2187499999999366618, 0.2499999999999214240, 0.4999999999999079625, 0.6249999999999011902, 0.6874999999998885336, 0.7187499999998855360, 0.7499999999998825384, 1.000000000000000000 ),
 .UNSPECIFIED. ) ;
#26164=EDGE_CURVE ( 'NONE', #25610, #3079, #17935, .T. ) ;
#26175=EDGE_LOOP ( 'NONE', ( #965, #1625, #12740, #10381 ) ) ;
#26218=DIRECTION ( 'NONE',  ( -1.000000000000000000, 0.000000000000000000, 0.000000000000000000 ) ) ;
#26275=CARTESIAN_POINT ( 'NONE',  ( -39.90867856081912635, -65.74137084430174127, -2.178535352963598015 ) ) ;
#26279=ORIENTED_EDGE ( 'NONE', *, *, #28542, .T. ) ;
#26300=CARTESIAN_POINT ( 'NONE',  ( -36.75091666766144982, -65.12255024416079152, 0.1339731005203242398 ) ) ;
#26308=CARTESIAN_POINT ( 'NONE',  ( -38.91454418380845937, -63.17361819573123682, 2.647414149835689567 ) ) ;
#26313=AXIS2_PLACEMENT_3D ( 'NONE', #20114, #4383, #24343 ) ;
#26318=DIRECTION ( 'NONE',  ( -0.5000000000009400258, 0.000000000000000000, -0.8660254037838960306 ) ) ;
#26320=LINE ( 'NONE', #6498, #651 ) ;
#26361=CARTESIAN_POINT ( 'NONE',  ( -38.25000000001202238, -63.17171877515667688, 2.272201163154965453 ) ) ;
#26398=LINE ( 'NONE', #6427, #24896 ) ;
#26414=VERTEX_POINT ( 'NONE', #11444 ) ;
#26433=AXIS2_PLACEMENT_3D ( 'NONE', #27589, #5562, #25255 ) ;
#26437=CARTESIAN_POINT ( 'NONE',  ( -36.70000763062214588, -65.09474816373202088, -0.01998728352818625667 ) ) ;
#26454=ADVANCED_FACE ( 'NONE', ( #7111 ), #2448, .T. ) ;
#26492=CARTESIAN_POINT ( 'NONE',  ( -42.17917380793182502, -65.66662781299496032, 0.7655265227419015828 ) ) ;
#26517=ADVANCED_FACE ( 'NONE', ( #17540 ), #46, .F. ) ;
#26530=CARTESIAN_POINT ( 'NONE',  ( -40.09372830037592195, -65.74402527486655856, 2.175418052786639134 ) ) ;
#26536=VERTEX_POINT ( 'NONE', #10807 ) ;
#26558=CARTESIAN_POINT ( 'NONE',  ( -42.12502810473512227, -65.68892072177348496, -0.8034381443789905264 ) ) ;
#26573=CARTESIAN_POINT ( 'NONE',  ( -40.00000000000000000, -63.40192378860000133, 0.000000000000000000 ) ) ;
#26579=CARTESIAN_POINT ( 'NONE',  ( -36.79999999999999716, -65.14977478849999670, -0.1732050807570000017 ) ) ;
#26582=CARTESIAN_POINT ( 'NONE',  ( -38.26719868119548806, -65.11500191527169079, -2.767150539682058152 ) ) ;
#26610=EDGE_CURVE ( 'NONE', #14702, #2354, #22646, .T. ) ;
#26633=CARTESIAN_POINT ( 'NONE',  ( -36.79999999999999716, -64.11445222650000630, -0.1732050807570000017 ) ) ;
#26645=ADVANCED_FACE ( 'NONE', ( #5304 ), #18688, .F. ) ;
#26651=EDGE_CURVE ( 'NONE', #14266, #20079, #19323, .T. ) ;
#26661=CARTESIAN_POINT ( 'NONE',  ( -38.85038231309999901, -65.31510159580000163, 2.684458023169999930 ) ) ;
#26671=CARTESIAN_POINT ( 'NONE',  ( -40.00000000000000000, -63.50000000000000000, 0.000000000000000000 ) ) ;
#26692=FACE_OUTER_BOUND ( 'NONE', #16176, .T. ) ;
#26700=CARTESIAN_POINT ( 'NONE',  ( -41.91080735079999897, -65.74290444429999525, -1.043878813350000101 ) ) ;
#26712=FACE_OUTER_BOUND ( 'NONE', #6769, .T. ) ;
#26713=FACE_OUTER_BOUND ( 'NONE', #18218, .T. ) ;
#26739=CARTESIAN_POINT ( 'NONE',  ( -38.45241897108094520, -65.10974319588028436, -2.885177897951406223 ) ) ;
#26740=CIRCLE ( 'NONE', #21611, 3.000000000000002665 ) ;
#26753=CARTESIAN_POINT ( 'NONE',  ( -41.75000000000000000, -63.30468293320000583, -1.587713240270000048 ) ) ;
#26761=DIRECTION ( 'NONE',  ( 0.000000000000000000, -1.000000000000000000, 0.000000000000000000 ) ) ;
#26780=ORIENTED_EDGE ( 'NONE', *, *, #14756, .T. ) ;
#26820=EDGE_LOOP ( 'NONE', ( #16721, #19613, #15995 ) ) ;
#26823=ORIENTED_EDGE ( 'NONE', *, *, #24213, .T. ) ;
#26825=CARTESIAN_POINT ( 'NONE',  ( -36.92846103339999786, -69.00000000000000000, 1.677989385109999843 ) ) ;
#26833=CARTESIAN_POINT ( 'NONE',  ( -40.00000000000000000, -63.00000000000000000, 0.000000000000000000 ) ) ;
#26838=DIRECTION ( 'NONE',  ( 0.4999999999997570277, 0.000000000000000000, 0.8660254037845789288 ) ) ;
#26893=ADVANCED_FACE ( 'NONE', ( #4527 ), #22465, .T. ) ;
#26895=EDGE_CURVE ( 'NONE', #19618, #17027, #9253, .T. ) ;
#26899=PLANE ( 'NONE',  #6035 ) ;
#26904=EDGE_LOOP ( 'NONE', ( #12789, #13109, #8359, #19201 ) ) ;
#26924=EDGE_CURVE ( 'NONE', #10539, #24995, #27578, .T. ) ;
#26979=DIRECTION ( 'NONE',  ( 1.000000000000000000, 0.000000000000000000, 0.000000000000000000 ) ) ;
#26987=CARTESIAN_POINT ( 'NONE',  ( -37.89761526037040795, -63.33348905331877177, -0.8208133671573618617 ) ) ;
#27000=AXIS2_PLACEMENT_3D ( 'NONE', #25548, #11988, #10213 ) ;
#27017=CARTESIAN_POINT ( 'NONE',  ( -36.71038433799841982, -63.05619511567397950, 0.07254510122748375478 ) ) ;
#27024=CARTESIAN_POINT ( 'NONE',  ( -38.04193375797715504, -65.73717265118393982, 0.9755880792773293786 ) ) ;
#27052=FACE_OUTER_BOUND ( 'NONE', #26175, .T. ) ;
#27064=CARTESIAN_POINT ( 'NONE',  ( -37.75000000000000000, -63.30468293320000583, 0.7216878364859999895 ) ) ;
#27072=AXIS2_PLACEMENT_3D ( 'NONE', #27716, #16764, #7476 ) ;
#27082=CARTESIAN_POINT ( 'NONE',  ( -38.25000000000000000, -64.47022873560000278, -1.587713240270000048 ) ) ;
#27093=AXIS2_PLACEMENT_3D ( 'NONE', #10128, #12599, #3593 ) ;
#27098=AXIS2_PLACEMENT_3D ( 'NONE', #27287, #9191, #13569 ) ;
#27099=DIRECTION ( 'NONE',  ( 0.5000000000001900702, 0.000000000000000000, -0.8660254037843290176 ) ) ;
#27125=CARTESIAN_POINT ( 'NONE',  ( -40.65756524500000069, -65.56519245710001087, -2.400371413390000264 ) ) ;
#27130=CARTESIAN_POINT ( 'NONE',  ( -38.23941415995982851, -65.68647126656233581, -1.441145490000594442 ) ) ;
#27161=CARTESIAN_POINT ( 'NONE',  ( -36.79999999999999716, -65.14977478849999670, -0.1732050807570000017 ) ) ;
#27189=CARTESIAN_POINT ( 'NONE',  ( -38.00919334667170091, -63.35144866725882196, 0.9204318061653798955 ) ) ;
#27198=CARTESIAN_POINT ( 'NONE',  ( -43.07153896660000214, -63.00000000000000000, -1.677989385109999843 ) ) ;
#27240=CARTESIAN_POINT ( 'NONE',  ( -43.20000000000000284, -63.00000000000000000, 0.1732050807559999961 ) ) ;
#27260=CARTESIAN_POINT ( 'NONE',  ( -41.75000000000000000, -65.63577453799999262, -1.587713240270000048 ) ) ;
#27263=ORIENTED_EDGE ( 'NONE', *, *, #16851, .T. ) ;
#27287=CARTESIAN_POINT ( 'NONE',  ( -40.00000000000000000, -66.00000000000000000, 0.000000000000000000 ) ) ;
#27315=CARTESIAN_POINT ( 'NONE',  ( -38.25000000000810729, -63.07121106306455260, -2.719955530748988881 ) ) ;
#27317=DIRECTION ( 'NONE',  ( 0.000000000000000000, 1.000000000000000000, 0.000000000000000000 ) ) ;
#27334=CARTESIAN_POINT ( 'NONE',  ( -40.50000000000000000, -63.30468293320000583, 2.309401076760000393 ) ) ;
#27397=FACE_OUTER_BOUND ( 'NONE', #28134, .T. ) ;
#27424=CARTESIAN_POINT ( 'NONE',  ( -38.25000000000000000, -63.30468293320000583, -1.587713240270000048 ) ) ;
#27425=CARTESIAN_POINT ( 'NONE',  ( -38.25000000000000000, -65.14977478849999670, -2.684678751729999480 ) ) ;
#27426=FACE_OUTER_BOUND ( 'NONE', #8294, .T. ) ;
#27435=FACE_OUTER_BOUND ( 'NONE', #20534, .T. ) ;
#27455=CARTESIAN_POINT ( 'NONE',  ( -43.29999236938066076, -65.09474816373038664, 0.01998728354478918057 ) ) ;
#27488=CARTESIAN_POINT ( 'NONE',  ( -41.45000000000000284, -63.07912966450000880, 2.857883832489999776 ) ) ;
#27504=CYLINDRICAL_SURFACE ( 'NONE', #15614, 0.9999999999999991118 ) ;
#27515=ORIENTED_EDGE ( 'NONE', *, *, #22877, .F. ) ;
#27519=EDGE_CURVE ( 'NONE', #767, #25860, #1481, .T. ) ;
#27530=VECTOR ( 'NONE', #2585, 1000.000000000000000 ) ;
#27531=ADVANCED_FACE ( 'NONE', ( #2592 ), #119, .T. ) ;
#27557=CYLINDRICAL_SURFACE ( 'NONE', #2583, 0.1999999999999996780 ) ;
#27563=CARTESIAN_POINT ( 'NONE',  ( -37.15721607020263662, -63.17171877515593792, -0.3794438750330945687 ) ) ;
#27564=CARTESIAN_POINT ( 'NONE',  ( -40.00000000000000000, -69.00000000000000000, 0.000000000000000000 ) ) ;
#27578=LINE ( 'NONE', #9909, #24231 ) ;
#27589=CARTESIAN_POINT ( 'NONE',  ( 0.000000000000000000, 0.000000000000000000, 0.000000000000000000 ) ) ;
#27617=CARTESIAN_POINT ( 'NONE',  ( -37.75000000000000000, -65.63577453799999262, 0.7216878364859999895 ) ) ;
#27628=DIRECTION ( 'NONE',  ( 0.000000000000000000, -1.000000000000000000, 0.000000000000000000 ) ) ;
#27644=FACE_OUTER_BOUND ( 'NONE', #7401, .T. ) ;
#27651=CARTESIAN_POINT ( 'NONE',  ( -40.00000000000000000, -65.00000000000000000, -3.175426480540000096 ) ) ;
#27653=CARTESIAN_POINT ( 'NONE',  ( -41.74999999999177902, -63.07121106306900771, 2.719955530729126991 ) ) ;
#27716=CARTESIAN_POINT ( 'NONE',  ( -41.54999999999999716, -65.00000000000000000, 2.684678751729999480 ) ) ;
#27722=CARTESIAN_POINT ( 'NONE',  ( -38.17164989577617007, -65.73761215452408635, 1.198860239814103057 ) ) ;
#27726=EDGE_CURVE ( 'NONE', #623, #21436, #6917, .T. ) ;
#27735=SURFACE_STYLE_USAGE ( .BOTH. , #5148 ) ;
#27743=DIRECTION ( 'NONE',  ( 0.000000000000000000, -1.000000000000000000, 0.000000000000000000 ) ) ;
#27751=CARTESIAN_POINT ( 'NONE',  ( -37.28811165380000148, -65.41419836839999391, 0.4550164754539999801 ) ) ;
#27809=CARTESIAN_POINT ( 'NONE',  ( -41.71910660533971082, -65.10668761693263207, -2.792605221528440929 ) ) ;
#27811=CARTESIAN_POINT ( 'NONE',  ( -41.81387021366961676, -65.73322674265565979, -1.234409484187863892 ) ) ;
#27841=CIRCLE ( 'NONE', #23212, 3.500000000000003109 ) ;
#27862=VERTEX_POINT ( 'NONE', #2697 ) ;
#27927=EDGE_LOOP ( 'NONE', ( #17414, #12987, #27515, #15123 ) ) ;
#27928=DIRECTION ( 'NONE',  ( 0.000000000000000000, 1.000000000000000000, 0.000000000000000000 ) ) ;
#27929=ADVANCED_FACE ( 'NONE', ( #18721 ), #14312, .F. ) ;
#27936=DIRECTION ( 'NONE',  ( 1.000000000000000000, 0.000000000000000000, 0.000000000000000000 ) ) ;
#27941=AXIS2_PLACEMENT_3D ( 'NONE', #11304, #9270, #18171 ) ;
#27968=ADVANCED_FACE ( 'NONE', ( #7658 ), #377, .F. ) ;
#27986=VECTOR ( 'NONE', #11260, 1000.000000000000000 ) ;
#28043=ORIENTED_EDGE ( 'NONE', *, *, #10109, .T. ) ;
#28057=CARTESIAN_POINT ( 'NONE',  ( -40.50000000000000000, -65.63577453799999262, 2.309401076760000393 ) ) ;
#28068=EDGE_LOOP ( 'NONE', ( #9381, #10599, #5221, #1909 ) ) ;
#28088=CARTESIAN_POINT ( 'NONE',  ( -41.75000000000000000, -65.63577453799999262, -1.587713240270000048 ) ) ;
#28103=CARTESIAN_POINT ( 'NONE',  ( -42.25000000000000000, -63.30468293320000583, 0.7216878364880000563 ) ) ;
#28105=VECTOR ( 'NONE', #8092, 1000.000000000000000 ) ;
#28134=EDGE_LOOP ( 'NONE', ( #14376, #6291, #26279, #2817, #25915, #15847 ) ) ;
#28144=CARTESIAN_POINT ( 'NONE',  ( -40.31253929845618700, -65.70258710782171363, 2.225363999267659043 ) ) ;
#28155=CARTESIAN_POINT ( 'NONE',  ( -41.75000000000000000, -65.63577453799999262, -1.587713240270000048 ) ) ;
#28169=CARTESIAN_POINT ( 'NONE',  ( -40.29219269051309027, -65.70788121356240197, -2.219015993087579464 ) ) ;
#28178=DIRECTION ( 'NONE',  ( 0.000000000000000000, -1.000000000000000000, 0.000000000000000000 ) ) ;
#28179=FACE_OUTER_BOUND ( 'NONE', #18408, .T. ) ;
#28191=DIRECTION ( 'NONE',  ( 0.000000000000000000, -1.000000000000000000, 0.000000000000000000 ) ) ;
#28199=B_SPLINE_CURVE_WITH_KNOTS ( 'NONE', 3,
 ( #26753, #10533, #19450, #28338 ),
 .UNSPECIFIED., .F., .F.,
 ( 4, 4 ),
 ( 0.000000000000000000, 1.000000000000000000 ),
 .UNSPECIFIED. ) ;
#28210=CARTESIAN_POINT ( 'NONE',  ( -40.50000000000000000, -63.30468293320000583, 2.309401076760000393 ) ) ;
#28271=CARTESIAN_POINT ( 'NONE',  ( -40.42662148796791399, -65.66662781299683616, 2.269983138304441095 ) ) ;
#28282=CARTESIAN_POINT ( 'NONE',  ( -40.00000000000000000, -94.00000000000000000, 0.000000000000000000 ) ) ;
#28338=CARTESIAN_POINT ( 'NONE',  ( -41.75000000000000000, -63.07912966450000880, -2.684678751739999925 ) ) ;
#28343=ORIENTED_EDGE ( 'NONE', *, *, #11528, .T. ) ;
#28347=CYLINDRICAL_SURFACE ( 'NONE', #1059, 0.9999999999999990008 ) ;
#28349=DIRECTION ( 'NONE',  ( 0.000000000000000000, -1.000000000000000000, 0.000000000000000000 ) ) ;
#28363=VERTEX_POINT ( 'NONE', #10736 ) ;
#28377=CARTESIAN_POINT ( 'NONE',  ( -41.75000000000000000, -63.30468293320000583, 1.587713240270000048 ) ) ;
#28390=VERTEX_POINT ( 'NONE', #8428 ) ;
#28438=VERTEX_POINT ( 'NONE', #24176 ) ;
#28447=CARTESIAN_POINT ( 'NONE',  ( -42.01869634261938558, -65.72281118314606374, -0.9050793633985121378 ) ) ;
#28462=CARTESIAN_POINT ( 'NONE',  ( -43.29972737720588327, -63.05366291736145001, 0.03679144966651182874 ) ) ;
#28468=CARTESIAN_POINT ( 'NONE',  ( -36.78600833567148953, -65.14196057590905298, 0.1651269895895124684 ) ) ;
#28485=EDGE_CURVE ( 'NONE', #6598, #12283, #19270, .T. ) ;
#28490=FACE_OUTER_BOUND ( 'NONE', #1206, .T. ) ;
#28519=CARTESIAN_POINT ( 'NONE',  ( -43.20000000000000284, -65.14977478849999670, -0.1732050807570000017 ) ) ;
#28542=EDGE_CURVE ( 'NONE', #22471, #21436, #16117, .T. ) ;
#28563=CARTESIAN_POINT ( 'NONE',  ( -40.28472764600749656, -65.70971443685482427, 2.216654594839819303 ) ) ;
#28611=CARTESIAN_POINT ( 'NONE',  ( -36.72757213148325661, -65.10974319588410708, -0.1023444634981215962 ) ) ;
#28617=EDGE_CURVE ( 'NONE', #2510, #18068, #20914, .T. ) ;
#28620=ORIENTED_EDGE ( 'NONE', *, *, #11877, .T. ) ;
#28626=ORIENTED_EDGE ( 'NONE', *, *, #18614, .F. ) ;
#28655=CARTESIAN_POINT ( 'NONE',  ( -41.86044139887496129, -65.74401284881750485, 1.128482062444109202 ) ) ;
#28735=CARTESIAN_POINT ( 'NONE',  ( -43.20000000000000284, -63.07912966450000880, -0.1732050807570000017 ) ) ;
#28757=ADVANCED_FACE ( 'NONE', ( #20281, #1941 ), #10782, .T. ) ;
#28778=ORIENTED_EDGE ( 'NONE', *, *, #26164, .T. ) ;
ENDSEC;
END-ISO-10303-21;
